ISO-10303-21;
HEADER;
FILE_DESCRIPTION (('STEP AP214'),
    '1' );
FILE_NAME ('hex flange nut gradea_iso_ISO - 4161 - M5 - N.step',
    '2026-10-08T13:56:24',
    ( '' ),
    ( '' ),
    'SwSTEP 2.0',
    'SolidWorks 2026',
    '' );
FILE_SCHEMA (( 'AUTOMOTIVE_DESIGN' ));
ENDSEC;

DATA;
#39=CARTESIAN_POINT ( 'NONE',  ( 4.197310751797292738, 0.8178363989516252985, -3.502498386812444409 ) ) ;
#96=CARTESIAN_POINT ( 'NONE',  ( -1.655952806101422814, 3.662737355149034979, -7.623296525288699970E-18 ) ) ;
#121=DIRECTION ( 'NONE',  ( 0.000000000000000000, -1.000000000000000000, 0.000000000000000000 ) ) ;
#134=DIRECTION ( 'NONE',  ( 1.000000000000000000, 0.000000000000000000, 0.000000000000000000 ) ) ;
#137=PRESENTATION_STYLE_ASSIGNMENT (( #9992 ) ) ;
#150=LINE ( 'NONE', #12166, #14801 ) ;
#154=ORIENTED_EDGE ( 'NONE', *, *, #781, .T. ) ;
#171=VECTOR ( 'NONE', #2459, 1000.000000000000114 ) ;
#173=CARTESIAN_POINT ( 'NONE',  ( -0.02511973781850462134, 4.877415612947412882, -3.751298745799839462 ) ) ;
#179=ORIENTED_EDGE ( 'NONE', *, *, #11221, .F. ) ;
#193=CARTESIAN_POINT ( 'NONE',  ( -4.000000000000000000, -2.309401076758512694, -5.000000000000000000 ) ) ;
#209=CARTESIAN_POINT ( 'NONE',  ( 4.000000000000000000, 0.3987449864460005378, -0.01220643443059817035 ) ) ;
#214=CARTESIAN_POINT ( 'NONE',  ( 4.211140560182196957, -2.431303136016555122, -3.745885042887436622 ) ) ;
#225=EDGE_LOOP ( 'NONE', ( #5891, #2747, #6648, #4937, #7254 ) ) ;
#236=DIRECTION ( 'NONE',  ( -0.8191520442889902442, 0.000000000000000000, -0.5735764363510482688 ) ) ;
#284=CARTESIAN_POINT ( 'NONE',  ( -5.560781378645573980, 0.000000000000000000, -4.000000000000000000 ) ) ;
#290=CARTESIAN_POINT ( 'NONE',  ( 4.000000000000000000, 0.7924765000094659007, -0.05906175389889852662 ) ) ;
#297=CARTESIAN_POINT ( 'NONE',  ( 8.673617379884035472E-16, 4.618802153517012954, 0.000000000000000000 ) ) ;
#316=EDGE_CURVE ( 'NONE', #15429, #4240, #2588, .T. ) ;
#337=CARTESIAN_POINT ( 'NONE',  ( -2.682243648011671588, -3.070208061305317759, -0.04852650426602272971 ) ) ;
#340=DIRECTION ( 'NONE',  ( 1.000000000000000000, 0.000000000000000000, 0.000000000000000000 ) ) ;
#348=CARTESIAN_POINT ( 'NONE',  ( 4.000000000000003553, -2.309401076758513138, -3.504271511726786859 ) ) ;
#360=CARTESIAN_POINT ( 'NONE',  ( 2.100000000000000089, 0.000000000000000000, -4.694516984716113228 ) ) ;
#390=CARTESIAN_POINT ( 'NONE',  ( -0.5636800770129166693, -4.293361309317430319, -3.531542292955206275 ) ) ;
#398=STYLED_ITEM ( 'NONE', ( #7612 ), #14732 ) ;
#405=CARTESIAN_POINT ( 'NONE',  ( -0.1404048886732797152, -4.699864953788083888, -3.686887068327043160 ) ) ;
#410=( GEOMETRIC_REPRESENTATION_CONTEXT ( 3 ) GLOBAL_UNCERTAINTY_ASSIGNED_CONTEXT ( ( #3205 ) ) GLOBAL_UNIT_ASSIGNED_CONTEXT ( ( #8747, #1452, #4035 ) ) REPRESENTATION_CONTEXT ( 'NONE', 'WORKASPACE' ) );
#411=CARTESIAN_POINT ( 'NONE',  ( -2.000000000000007550, -3.464101615137749945, 0.000000000000000000 ) ) ;
#444=CIRCLE ( 'NONE', #3775, 5.560781378645573980 ) ;
#448=UNCERTAINTY_MEASURE_WITH_UNIT (LENGTH_MEASURE( 1.000000000000000082E-05 ), #1256, 'distance_accuracy_value', 'NONE');
#457=CARTESIAN_POINT ( 'NONE',  ( -2.500000000000000444, 3.061616997868383634E-16, -25.03750572909317285 ) ) ;
#458=ORIENTED_EDGE ( 'NONE', *, *, #13196, .F. ) ;
#463=CARTESIAN_POINT ( 'NONE',  ( -1.360585162435467455, 4.061296242128285883, -3.505054077164959203 ) ) ;
#473=EDGE_CURVE ( 'NONE', #8001, #6278, #15322, .T. ) ;
#572=DIRECTION ( 'NONE',  ( 0.000000000000000000, 0.000000000000000000, 1.000000000000000000 ) ) ;
#579=CARTESIAN_POINT ( 'NONE',  ( 3.511755186886750923, -2.826662030176382956, -3.597382984111582083 ) ) ;
#678=VERTEX_POINT ( 'NONE', #1212 ) ;
#687=CARTESIAN_POINT ( 'NONE',  ( 0.000000000000000000, 0.000000000000000000, -5.000000000000000000 ) ) ;
#705=DIRECTION ( 'NONE',  ( -1.000000000000000000, 0.000000000000000000, 0.000000000000000000 ) ) ;
#732=CARTESIAN_POINT ( 'NONE',  ( 2.500000000000000444, 0.000000000000000000, -25.03750572909317285 ) ) ;
#746=CARTESIAN_POINT ( 'NONE',  ( -4.101948962585905356, -2.368261337751088824, -3.681124513963624167 ) ) ;
#749=FACE_OUTER_BOUND ( 'NONE', #2270, .T. ) ;
#781=EDGE_CURVE ( 'NONE', #5812, #14017, #1873, .T. ) ;
#806=DIRECTION ( 'NONE',  ( -0.000000000000000000, -0.000000000000000000, 1.000000000000000000 ) ) ;
#817=EDGE_LOOP ( 'NONE', ( #5789, #2864, #13408 ) ) ;
#847=EDGE_LOOP ( 'NONE', ( #5663, #1091, #13175, #4409, #14855 ) ) ;
#860=DIRECTION ( 'NONE',  ( -1.000000000000000000, 0.000000000000000000, 0.000000000000000000 ) ) ;
#873=PRODUCT ( 'hex flange nut gradea_iso_ISO - 4161 - M5 - N', 'hex flange nut gradea_iso_ISO - 4161 - M5 - N', '', ( #14449 ) ) ;
#876=CARTESIAN_POINT ( 'NONE',  ( -3.861362476283256129, -2.629030857716004199, -3.671615880910374941 ) ) ;
#893=CARTESIAN_POINT ( 'NONE',  ( -3.999999999999999112, 1.539600717838996324, -3.300726591567078039 ) ) ;
#955=CARTESIAN_POINT ( 'NONE',  ( 1.734723475976807094E-15, 4.618802153517012954, -0.4999999999999995559 ) ) ;
#972=ORIENTED_EDGE ( 'NONE', *, *, #6643, .F. ) ;
#981=CARTESIAN_POINT ( 'NONE',  ( 3.540020015735602765, 2.810662092924382627, -3.602146406945867962 ) ) ;
#982=CARTESIAN_POINT ( 'NONE',  ( 0.6666666666666689611, 4.233901974057261874, -3.300726591567082480 ) ) ;
#994=VECTOR ( 'NONE', #10000, 1000.000000000000000 ) ;
#998=CARTESIAN_POINT ( 'NONE',  ( 3.510273485745307731, 2.827716139362654424, -3.610536846335885564 ) ) ;
#1040=EDGE_LOOP ( 'NONE', ( #12922, #2165, #8177, #15346 ) ) ;
#1055=FACE_OUTER_BOUND ( 'NONE', #5659, .T. ) ;
#1057=EDGE_CURVE ( 'NONE', #5664, #15429, #10141, .T. ) ;
#1074=CARTESIAN_POINT ( 'NONE',  ( 4.204115023516791005, -1.660442669500199919, -3.602151381774560068 ) ) ;
#1091=ORIENTED_EDGE ( 'NONE', *, *, #10222, .T. ) ;
#1104=DIRECTION ( 'NONE',  ( 0.000000000000000000, 0.000000000000000000, 1.000000000000000000 ) ) ;
#1112=ORIENTED_EDGE ( 'NONE', *, *, #2548, .T. ) ;
#1122=CARTESIAN_POINT ( 'NONE',  ( 0.000000000000000000, 0.000000000000000000, 0.000000000000000000 ) ) ;
#1126=EDGE_CURVE ( 'NONE', #5812, #2885, #10679, .T. ) ;
#1130=DIRECTION ( 'NONE',  ( 1.000000000000000000, 0.000000000000000000, 0.000000000000000000 ) ) ;
#1151=B_SPLINE_CURVE_WITH_KNOTS ( 'NONE', 3,
 ( #1741, #5774, #12799, #10712, #5703 ),
 .UNSPECIFIED., .F., .F.,
 ( 4, 1, 4 ),
 ( 0.000000000000000000, 0.002309401076758505790, 0.004618802153517011580 ),
 .UNSPECIFIED. ) ;
#1212=CARTESIAN_POINT ( 'NONE',  ( 4.000000000000000000, 2.309401076758497151, -3.433295621305379353 ) ) ;
#1246=CARTESIAN_POINT ( 'NONE',  ( -2.000000000000007550, -3.464101615137749945, 0.000000000000000000 ) ) ;
#1253=AXIS2_PLACEMENT_3D ( 'NONE', #297, #13847, #4963 ) ;
#1256=( LENGTH_UNIT ( ) NAMED_UNIT ( * ) SI_UNIT ( .MILLI., .METRE. ) );
#1257=ORIENTED_EDGE ( 'NONE', *, *, #4707, .F. ) ;
#1262=B_SPLINE_CURVE_WITH_KNOTS ( 'NONE', 3,
 ( #15673, #10735, #9525, #12006, #6785, #4434 ),
 .UNSPECIFIED., .F., .F.,
 ( 4, 2, 4 ),
 ( -3.640115492407174633E-06, 0.0002066546034006553863, 0.0004169493222937179812 ),
 .UNSPECIFIED. ) ;
#1272=ORIENTED_EDGE ( 'NONE', *, *, #15927, .T. ) ;
#1284=CARTESIAN_POINT ( 'NONE',  ( -0.6448876103708541807, -4.246476118072358474, -0.2256878752776773356 ) ) ;
#1298=ADVANCED_FACE ( 'NONE', ( #12183 ), #6541, .T. ) ;
#1334=ORIENTED_EDGE ( 'NONE', *, *, #11046, .T. ) ;
#1350=ORIENTED_EDGE ( 'NONE', *, *, #12395, .F. ) ;
#1375=CARTESIAN_POINT ( 'NONE',  ( 4.197393957002303999, 7.772902908466098641E-14, -3.503767560748929810 ) ) ;
#1396=CARTESIAN_POINT ( 'NONE',  ( -2.687328764639638656, 3.067272167851286202, -0.05923475698270370959 ) ) ;
#1406=EDGE_LOOP ( 'NONE', ( #6205, #15290, #10257, #9032, #4103 ) ) ;
#1426=CARTESIAN_POINT ( 'NONE',  ( 0.02511973781850649831, -4.877415612947427981, -3.751298745799844792 ) ) ;
#1432=ORIENTED_EDGE ( 'NONE', *, *, #15632, .T. ) ;
#1438=CARTESIAN_POINT ( 'NONE',  ( -4.000000000000000000, -1.560351142792950618, -0.2242961665059814425 ) ) ;
#1452=( NAMED_UNIT ( * ) PLANE_ANGLE_UNIT ( ) SI_UNIT ( $, .RADIAN. ) );
#1486=EDGE_CURVE ( 'NONE', #15428, #15685, #1262, .T. ) ;
#1490=PLANE ( 'NONE',  #2529 ) ;
#1510=CARTESIAN_POINT ( 'NONE',  ( 2.059999999999998721, 0.000000000000000000, -0.3080913168122742518 ) ) ;
#1511=AXIS2_PLACEMENT_3D ( 'NONE', #4494, #9429, #860 ) ;
#1565=CARTESIAN_POINT ( 'NONE',  ( 2.100000000000000089, 0.000000000000000000, -0.2800830152838844622 ) ) ;
#1566=DIRECTION ( 'NONE',  ( 0.8660254037844379305, 0.5000000000000013323, 0.000000000000000000 ) ) ;
#1577=CARTESIAN_POINT ( 'NONE',  ( -4.197393957002303999, -7.773935952363655451E-14, -3.503767560748929810 ) ) ;
#1580=VERTEX_POINT ( 'NONE', #955 ) ;
#1595=ORIENTED_EDGE ( 'NONE', *, *, #11836, .F. ) ;
#1607=LINE ( 'NONE', #6632, #11168 ) ;
#1613=CARTESIAN_POINT ( 'NONE',  ( 2.100000000000000089, 0.000000000000000000, -5.000000000000000000 ) ) ;
#1621=DIRECTION ( 'NONE',  ( 0.000000000000000000, 0.000000000000000000, 1.000000000000000000 ) ) ;
#1656=CARTESIAN_POINT ( 'NONE',  ( -0.5276280594146446346, 4.314175951381965746, -3.320322319201721495 ) ) ;
#1666=CARTESIAN_POINT ( 'NONE',  ( -2.742827927723112236, -3.035229711105190464, -3.433252694550595230 ) ) ;
#1682=ADVANCED_FACE ( 'NONE', ( #10964 ), #2635, .T. ) ;
#1701=CIRCLE ( 'NONE', #14866, 4.000000000000000000 ) ;
#1721=CARTESIAN_POINT ( 'NONE',  ( -2.688821387764050996E-14, -4.618802153517012954, -0.4999999999999995559 ) ) ;
#1731=DIRECTION ( 'NONE',  ( 1.000000000000000000, 0.000000000000000000, 0.000000000000000000 ) ) ;
#1739=CARTESIAN_POINT ( 'NONE',  ( -2.712762565639006418, 3.052587955997511759, -3.430618716626627318 ) ) ;
#1741=CARTESIAN_POINT ( 'NONE',  ( 4.000000000000000000, -2.309401076758514915, -3.433295621305383349 ) ) ;
#1765=CONICAL_SURFACE ( 'NONE', #10292, 4.000000000000000000, 0.8911886515913786111 ) ;
#1831=ORIENTED_EDGE ( 'NONE', *, *, #11856, .T. ) ;
#1873=CIRCLE ( 'NONE', #7573, 2.100000000000000089 ) ;
#1878=ADVANCED_FACE ( 'NONE', ( #8145 ), #4490, .T. ) ;
#1894=DIRECTION ( 'NONE',  ( 1.000000000000000000, 0.000000000000000000, 0.000000000000000000 ) ) ;
#1898=CARTESIAN_POINT ( 'NONE',  ( -4.000000000000000000, -2.309401076758515803, -0.4999999999999995559 ) ) ;
#1899=DIRECTION ( 'NONE',  ( -0.8660254037844373753, 0.5000000000000021094, 0.000000000000000000 ) ) ;
#1900=CARTESIAN_POINT ( 'NONE',  ( 4.000000000000000000, -2.309401076758516691, -0.4999999999999995559 ) ) ;
#1922=DIRECTION ( 'NONE',  ( 1.000000000000000000, 0.000000000000000000, 0.000000000000000000 ) ) ;
#1932=CARTESIAN_POINT ( 'NONE',  ( 0.3461262719736147297, -4.658553426539303821, -3.671615880910379381 ) ) ;
#1976=ORIENTED_EDGE ( 'NONE', *, *, #8220, .F. ) ;
#1991=ORIENTED_EDGE ( 'NONE', *, *, #9830, .F. ) ;
#2021=CARTESIAN_POINT ( 'NONE',  ( -4.000000000000000000, 2.309401076758498483, -0.4999999999999927280 ) ) ;
#2032=CARTESIAN_POINT ( 'NONE',  ( 4.204015924366189871, -1.626724848190933548, -3.610627190413393084 ) ) ;
#2048=CARTESIAN_POINT ( 'NONE',  ( 1.411581201560190495E-15, 4.862606272033091592, -3.745885042887436622 ) ) ;
#2052=CARTESIAN_POINT ( 'NONE',  ( -6.259644161404860030E-16, -4.618802153517027165, -3.433295621305388234 ) ) ;
#2053=LINE ( 'NONE', #10784, #5284 ) ;
#2089=EDGE_LOOP ( 'NONE', ( #1432, #8925, #11103, #12155 ) ) ;
#2101=B_SPLINE_CURVE_WITH_KNOTS ( 'NONE', 3,
 ( #12103, #893, #12174, #4758, #10981 ),
 .UNSPECIFIED., .F., .F.,
 ( 4, 1, 4 ),
 ( 0.000000000000000000, 0.002309401076758505790, 0.004618802153517011580 ),
 .UNSPECIFIED. ) ;
#2162=ORIENTED_EDGE ( 'NONE', *, *, #14228, .T. ) ;
#2165=ORIENTED_EDGE ( 'NONE', *, *, #5262, .T. ) ;
#2183=CARTESIAN_POINT ( 'NONE',  ( -4.211140560182196957, -2.431303136016552013, -3.745885042887436178 ) ) ;
#2189=AXIS2_PLACEMENT_3D ( 'NONE', #687, #5615, #1130 ) ;
#2196=VECTOR ( 'NONE', #11552, 1000.000000000000000 ) ;
#2201=CARTESIAN_POINT ( 'NONE',  ( 2.500000000000000444, 0.000000000000000000, -5.000000000000000888 ) ) ;
#2209=CONICAL_SURFACE ( 'NONE', #8183, 4.000000000000000000, 0.8911886515913786111 ) ;
#2211=TOROIDAL_SURFACE ( 'NONE', #11252, 5.384454397937118664, 0.5155456020628804703 ) ;
#2270=EDGE_LOOP ( 'NONE', ( #10617, #3870, #9843, #1976 ) ) ;
#2298=CARTESIAN_POINT ( 'NONE',  ( -2.345747346278108214, 3.264484291692489215, -0.01223254789873409049 ) ) ;
#2337=CARTESIAN_POINT ( 'NONE',  ( 4.154306624731137099, 2.398490048084935822, -3.721999068284414847 ) ) ;
#2357=CARTESIAN_POINT ( 'NONE',  ( 2.449848172108560096, 3.432307619358740514, -3.503702292528905637 ) ) ;
#2359=EDGE_LOOP ( 'NONE', ( #6420, #458, #6480 ) ) ;
#2360=CARTESIAN_POINT ( 'NONE',  ( 4.000000000000000000, -2.471525695159793035, -3.686886880705770864 ) ) ;
#2366=ADVANCED_FACE ( 'NONE', ( #749 ), #6545, .F. ) ;
#2377=FACE_OUTER_BOUND ( 'NONE', #6162, .T. ) ;
#2383=DIRECTION ( 'NONE',  ( 1.000000000000000000, 0.000000000000000000, 0.000000000000000000 ) ) ;
#2408=CARTESIAN_POINT ( 'NONE',  ( -6.473970235329672780E-16, -4.862606272033106691, -3.745885042887442395 ) ) ;
#2417=CARTESIAN_POINT ( 'NONE',  ( -2.000000000000006661, 3.464101615137750834, 0.000000000000000000 ) ) ;
#2434=CARTESIAN_POINT ( 'NONE',  ( 4.000000000000000000, -1.700175430507292473, -3.320327275037661785 ) ) ;
#2439=B_SPLINE_CURVE_WITH_KNOTS ( 'NONE', 3,
 ( #14004, #5287, #15068, #3985, #7738 ),
 .UNSPECIFIED., .F., .F.,
 ( 4, 1, 4 ),
 ( 5.640274452250024914E-20, 0.002309401076758505356, 0.004618802153517010713 ),
 .UNSPECIFIED. ) ;
#2440=CARTESIAN_POINT ( 'NONE',  ( -3.355112389629170799, 2.681727112203152963, -0.2256878752776689534 ) ) ;
#2459=DIRECTION ( 'NONE',  ( 0.8191520442889902442, 1.003171929053522651E-16, -0.5735764363510482688 ) ) ;
#2483=DIRECTION ( 'NONE',  ( -0.8660254037844377084, -0.5000000000000015543, 0.000000000000000000 ) ) ;
#2500=EDGE_CURVE ( 'NONE', #6278, #8001, #10693, .T. ) ;
#2514=CARTESIAN_POINT ( 'NONE',  ( 4.197478902586992966, -0.8524102783748346290, -3.505063281295504041 ) ) ;
#2529=AXIS2_PLACEMENT_3D ( 'NONE', #4066, #2850, #1566 ) ;
#2548=EDGE_CURVE ( 'NONE', #678, #14655, #1607, .T. ) ;
#2559=PLANE ( 'NONE',  #3238 ) ;
#2569=EDGE_CURVE ( 'NONE', #3401, #4698, #7429, .T. ) ;
#2582=ORIENTED_EDGE ( 'NONE', *, *, #10966, .T. ) ;
#2584=ORIENTED_EDGE ( 'NONE', *, *, #13761, .T. ) ;
#2586=ORIENTED_EDGE ( 'NONE', *, *, #1126, .F. ) ;
#2588=B_SPLINE_CURVE_WITH_KNOTS ( 'NONE', 3,
 ( #10155, #6448, #9187, #8948, #6596 ),
 .UNSPECIFIED., .F., .F.,
 ( 4, 1, 4 ),
 ( 0.000000000000000000, 0.002309401076758505356, 0.004618802153517010713 ),
 .UNSPECIFIED. ) ;
#2599=EDGE_CURVE ( 'NONE', #7177, #15428, #8011, .T. ) ;
#2625=FILL_AREA_STYLE_COLOUR ( '', #6323 ) ;
#2635=CONICAL_SURFACE ( 'NONE', #14525, 4.000000000000000000, 0.8911886515913786111 ) ;
#2649=FACE_OUTER_BOUND ( 'NONE', #11353, .T. ) ;
#2650=DIRECTION ( 'NONE',  ( 1.000000000000000000, 0.000000000000000000, 0.000000000000000000 ) ) ;
#2667=ORIENTED_EDGE ( 'NONE', *, *, #3812, .F. ) ;
#2675=EDGE_LOOP ( 'NONE', ( #11553, #9109, #13096, #1257 ) ) ;
#2691=CARTESIAN_POINT ( 'NONE',  ( 1.567478505476134606E-15, 4.618802153517012066, -3.433295621305382905 ) ) ;
#2699=B_SPLINE_CURVE_WITH_KNOTS ( 'NONE', 3,
 ( #4885, #8611, #209, #290, #9969, #14910, #10220, #9885 ),
 .UNSPECIFIED., .F., .F.,
 ( 4, 2, 2, 4 ),
 ( 0.005725059856848645212, 0.006314084072593634418, 0.006903108288338624492, 0.008081156719828603771 ),
 .UNSPECIFIED. ) ;
#2715=CARTESIAN_POINT ( 'NONE',  ( -4.140404888673278272, -2.228338276487456415, -3.686887068327035166 ) ) ;
#2743=EDGE_LOOP ( 'NONE', ( #11065, #6512 ) ) ;
#2747=ORIENTED_EDGE ( 'NONE', *, *, #316, .T. ) ;
#2755=ADVANCED_FACE ( 'NONE', ( #5575 ), #5013, .T. ) ;
#2777=CARTESIAN_POINT ( 'NONE',  ( -3.333333333333335258, 2.694301256218251783, -3.300726591567079815 ) ) ;
#2816=CARTESIAN_POINT ( 'NONE',  ( 0.5276280594147412240, -4.314175951381924889, -3.320322319201654881 ) ) ;
#2846=ADVANCED_FACE ( 'NONE', ( #11127 ), #4761, .F. ) ;
#2850=DIRECTION ( 'NONE',  ( 0.5000000000000013323, -0.8660254037844379305, 0.000000000000000000 ) ) ;
#2851=DIRECTION ( 'NONE',  ( -1.000000000000000000, 0.000000000000000000, 0.000000000000000000 ) ) ;
#2852=UNCERTAINTY_MEASURE_WITH_UNIT (LENGTH_MEASURE( 1.000000000000000082E-05 ), #5957, 'distance_accuracy_value', 'NONE');
#2864=ORIENTED_EDGE ( 'NONE', *, *, #13988, .T. ) ;
#2872=B_SPLINE_CURVE_WITH_KNOTS ( 'NONE', 3,
 ( #5428, #579, #5665, #10360, #14389, #9148, #1932, #10433 ),
 .UNSPECIFIED., .F., .F.,
 ( 4, 2, 2, 4 ),
 ( 0.000000000000000000, 0.002450665683189819262, 0.003675998524784728893, 0.004901331366379639391 ),
 .UNSPECIFIED. ) ;
#2885=VERTEX_POINT ( 'NONE', #3529 ) ;
#2890=CARTESIAN_POINT ( 'NONE',  ( 0.000000000000000000, 0.000000000000000000, -4.484454397937119197 ) ) ;
#2910=PLANE ( 'NONE',  #3278 ) ;
#2916=EDGE_CURVE ( 'NONE', #4240, #15626, #150, .T. ) ;
#2939=CARTESIAN_POINT ( 'NONE',  ( -4.000000000000000000, 0.8576368993457507139, -3.433240632782198709 ) ) ;
#2993=FACE_OUTER_BOUND ( 'NONE', #3292, .T. ) ;
#2997=B_SPLINE_CURVE_WITH_KNOTS ( 'NONE', 3,
 ( #12779, #15554, #15312, #8046, #13020, #1721 ),
 .UNSPECIFIED., .F., .F.,
 ( 4, 2, 4 ),
 ( 0.002365888236227967761, 0.003551327329835077609, 0.004736766423442186590 ),
 .UNSPECIFIED. ) ;
#3004=B_SPLINE_CURVE_WITH_KNOTS ( 'NONE', 3,
 ( #9935, #6065, #13556, #982, #14874 ),
 .UNSPECIFIED., .F., .F.,
 ( 4, 1, 4 ),
 ( 0.000000000000000000, 0.002309401076758505356, 0.004618802153517010713 ),
 .UNSPECIFIED. ) ;
#3008=DIRECTION ( 'NONE',  ( 1.000000000000000000, 0.000000000000000000, 0.000000000000000000 ) ) ;
#3011=ADVANCED_FACE ( 'NONE', ( #5473 ), #14003, .T. ) ;
#3028=CARTESIAN_POINT ( 'NONE',  ( -4.211399284164270895, 2.459729995988205964, -3.751162237960538715 ) ) ;
#3037=VECTOR ( 'NONE', #9374, 1000.000000000000000 ) ;
#3038=B_SPLINE_CURVE_WITH_KNOTS ( 'NONE', 3,
 ( #8252, #13503, #2440, #14822, #1396, #2298, #5043, #8776 ),
 .UNSPECIFIED., .F., .F.,
 ( 4, 2, 2, 4 ),
 ( 2.465131517071352357E-07, 0.001183067374689843057, 0.001774477805458910071, 0.002365888236227977302 ),
 .UNSPECIFIED. ) ;
#3059=CARTESIAN_POINT ( 'NONE',  ( -2.449848172108560540, -3.432307619358754724, -3.503702292528910078 ) ) ;
#3071=CARTESIAN_POINT ( 'NONE',  ( -3.679171394226034675, -2.494631558665844739, -0.3503314178412558211 ) ) ;
#3090=DIRECTION ( 'NONE',  ( -1.000000000000000000, 0.000000000000000000, 0.000000000000000000 ) ) ;
#3111=CARTESIAN_POINT ( 'NONE',  ( 4.000000000000000000, 2.309401076758515803, -0.4999999999999995559 ) ) ;
#3153=ORIENTED_EDGE ( 'NONE', *, *, #7920, .T. ) ;
#3161=CARTESIAN_POINT ( 'NONE',  ( 0.5636800770130377947, 4.293361309317166530, -3.531542292954102713 ) ) ;
#3194=FACE_OUTER_BOUND ( 'NONE', #2089, .T. ) ;
#3205=UNCERTAINTY_MEASURE_WITH_UNIT (LENGTH_MEASURE( 1.000000000000000082E-05 ), #8747, 'distance_accuracy_value', 'NONE');
#3210=CARTESIAN_POINT ( 'NONE',  ( -4.211140560182196957, -2.431303136016552013, -3.745885042887436178 ) ) ;
#3223=AXIS2_PLACEMENT_3D ( 'NONE', #11897, #11972, #4638 ) ;
#3233=EDGE_LOOP ( 'NONE', ( #11734, #9232 ) ) ;
#3238=AXIS2_PLACEMENT_3D ( 'NONE', #193, #12336, #7344 ) ;
#3255=EDGE_CURVE ( 'NONE', #3401, #5290, #15711, .T. ) ;
#3261=CLOSED_SHELL ( 'NONE', ( #3737, #8881, #9193, #3011, #2755, #15614, #5700, #9905, #1878, #12640, #6913, #15117, #13782, #7901, #9643, #11723, #15235, #6986, #6620, #1682, #1298, #15595, #8679, #8814, #13135, #10346, #10652, #12433, #2366, #2846, #5245, #15947 ) ) ;
#3278=AXIS2_PLACEMENT_3D ( 'NONE', #6733, #15049, #1621 ) ;
#3292=EDGE_LOOP ( 'NONE', ( #5754, #2584, #1112, #4327, #5277 ) ) ;
#3293=ORIENTED_EDGE ( 'NONE', *, *, #11906, .F. ) ;
#3310=ORIENTED_EDGE ( 'NONE', *, *, #2500, .F. ) ;
#3337=CARTESIAN_POINT ( 'NONE',  ( -4.000000000000000000, 0.7924765000094600165, -0.05906175389889745803 ) ) ;
#3340=FACE_OUTER_BOUND ( 'NONE', #2359, .T. ) ;
#3344=LINE ( 'NONE', #8208, #12889 ) ;
#3350=B_SPLINE_CURVE_WITH_KNOTS ( 'NONE', 3,
 ( #2048, #4792, #12131, #2357, #3488, #998, #4635, #5932 ),
 .UNSPECIFIED., .F., .F.,
 ( 4, 2, 2, 4 ),
 ( 7.780516681398759253E-20, 0.002450665683189819696, 0.003675998524784729327, 0.004901331366379639391 ),
 .UNSPECIFIED. ) ;
#3370=EDGE_LOOP ( 'NONE', ( #12716, #13421, #1272, #11790, #2582 ) ) ;
#3398=B_SPLINE_CURVE_WITH_KNOTS ( 'NONE', 3,
 ( #7716, #8763, #11166, #7793 ),
 .UNSPECIFIED., .F., .F.,
 ( 4, 4 ),
 ( 0.000000000000000000, 0.002452478801916361129 ),
 .UNSPECIFIED. ) ;
#3401=VERTEX_POINT ( 'NONE', #1246 ) ;
#3406=CARTESIAN_POINT ( 'NONE',  ( 0.000000000000000000, 0.000000000000000000, 0.000000000000000000 ) ) ;
#3416=DIRECTION ( 'NONE',  ( 1.000000000000000000, 0.000000000000000000, 0.000000000000000000 ) ) ;
#3423=AXIS2_PLACEMENT_3D ( 'NONE', #12803, #5548, #1899 ) ;
#3466=FACE_OUTER_BOUND ( 'NONE', #9360, .T. ) ;
#3473=CARTESIAN_POINT ( 'NONE',  ( 4.211140560182196957, -2.431303136016555122, -3.745885042887436622 ) ) ;
#3479=ORIENTED_EDGE ( 'NONE', *, *, #9313, .T. ) ;
#3488=CARTESIAN_POINT ( 'NONE',  ( 2.804994570502171047, 3.229033611042449792, -3.526374918436834704 ) ) ;
#3503=CARTESIAN_POINT ( 'NONE',  ( 4.211140560182196957, 2.431303136016536470, -3.745885042887433514 ) ) ;
#3512=EDGE_CURVE ( 'NONE', #4240, #10129, #2439, .T. ) ;
#3529=CARTESIAN_POINT ( 'NONE',  ( -2.499999999999999556, 3.061616997868382648E-16, 3.469446951953614189E-15 ) ) ;
#3546=CARTESIAN_POINT ( 'NONE',  ( -1.312671235360383548, -3.860931062424228788, -0.05923475698271369466 ) ) ;
#3563=AXIS2_PLACEMENT_3D ( 'NONE', #10513, #8093, #4438 ) ;
#3585=CARTESIAN_POINT ( 'NONE',  ( 4.000000000000000000, -0.8732470631449981147, -3.223155494240760088 ) ) ;
#3602=CARTESIAN_POINT ( 'NONE',  ( -4.211140560182196957, 2.431303136016537803, -3.745885042887433514 ) ) ;
#3647=EDGE_CURVE ( 'NONE', #7141, #11376, #3344, .T. ) ;
#3676=DIRECTION ( 'NONE',  ( -1.000000000000000000, 0.000000000000000000, 0.000000000000000000 ) ) ;
#3680=ORIENTED_EDGE ( 'NONE', *, *, #12862, .T. ) ;
#3704=DIRECTION ( 'NONE',  ( -1.000000000000000000, 0.000000000000000000, 0.000000000000000000 ) ) ;
#3735=CARTESIAN_POINT ( 'NONE',  ( 4.000000000000000000, 0.8378280264232961239, -3.220590601395640018 ) ) ;
#3737=ADVANCED_FACE ( 'NONE', ( #10931 ), #6004, .F. ) ;
#3775=AXIS2_PLACEMENT_3D ( 'NONE', #11513, #4244, #1894 ) ;
#3782=CARTESIAN_POINT ( 'NONE',  ( -3.999999999998910649, -1.658469974638591804, -3.531532913075256186 ) ) ;
#3796=CIRCLE ( 'NONE', #14905, 2.499999999999999556 ) ;
#3812=EDGE_CURVE ( 'NONE', #7875, #12489, #3398, .T. ) ;
#3831=CARTESIAN_POINT ( 'NONE',  ( -5.384454397937118664, 6.702023979852544604E-16, -5.000000000000000000 ) ) ;
#3843=CARTESIAN_POINT ( 'NONE',  ( -4.101948962585906244, 2.368261337751074169, -3.681124513963621503 ) ) ;
#3844=ORIENTED_EDGE ( 'NONE', *, *, #5702, .F. ) ;
#3853=EDGE_CURVE ( 'NONE', #5290, #11740, #4337, .T. ) ;
#3870=ORIENTED_EDGE ( 'NONE', *, *, #9426, .F. ) ;
#3878=CARTESIAN_POINT ( 'NONE',  ( -0.1756481739660520902, 4.720212674038980261, -3.469390959564065291 ) ) ;
#3916=CARTESIAN_POINT ( 'NONE',  ( -4.000000000000000000, 2.309401076758498483, -3.433295621305379353 ) ) ;
#3932=FACE_OUTER_BOUND ( 'NONE', #9636, .T. ) ;
#3945=CARTESIAN_POINT ( 'NONE',  ( 1.243802165048773611, -3.900692638707475624, -3.223146290109810241 ) ) ;
#3958=B_SPLINE_CURVE_WITH_KNOTS ( 'NONE', 3,
 ( #7600, #12497, #1438, #6386, #7684, #11304 ),
 .UNSPECIFIED., .F., .F.,
 ( 4, 2, 4 ),
 ( 0.003358874760055550156, 0.004541967308452096383, 0.005725059856848641743 ),
 .UNSPECIFIED. ) ;
#3969=CARTESIAN_POINT ( 'NONE',  ( 0.000000000000000000, 0.000000000000000000, 0.000000000000000000 ) ) ;
#3970=ORIENTED_EDGE ( 'NONE', *, *, #14575, .F. ) ;
#3985=CARTESIAN_POINT ( 'NONE',  ( 3.333333333333335702, -2.694301256218268215, -3.300726591567084256 ) ) ;
#3991=CARTESIAN_POINT ( 'NONE',  ( -4.211140560182196957, 2.431303136016537803, -3.745885042887433514 ) ) ;
#3992=DIRECTION ( 'NONE',  ( -0.000000000000000000, -0.000000000000000000, 1.000000000000000000 ) ) ;
#4008=CARTESIAN_POINT ( 'NONE',  ( -3.540020015735593439, -2.810662092924100630, -3.602146406945814672 ) ) ;
#4015=ORIENTED_EDGE ( 'NONE', *, *, #13061, .F. ) ;
#4029=CARTESIAN_POINT ( 'NONE',  ( -2.805705207896067144, 3.226868319750155312, -3.503898532754364581 ) ) ;
#4035=( NAMED_UNIT ( * ) SI_UNIT ( $, .STERADIAN. ) SOLID_ANGLE_UNIT ( ) );
#4050=PRODUCT_DEFINITION_FORMATION_WITH_SPECIFIED_SOURCE ( 'ANY', '', #873, .NOT_KNOWN. ) ;
#4051=EDGE_CURVE ( 'NONE', #5600, #7177, #10162, .T. ) ;
#4066=CARTESIAN_POINT ( 'NONE',  ( -6.259644161404860030E-16, -4.618802153517027165, -5.000000000000000000 ) ) ;
#4095=CARTESIAN_POINT ( 'NONE',  ( -2.836893136758495970, -3.208949435745868328, -3.505054077164885484 ) ) ;
#4103=ORIENTED_EDGE ( 'NONE', *, *, #9313, .F. ) ;
#4158=CARTESIAN_POINT ( 'NONE',  ( -4.000000000000000000, 1.700094919196744270, -3.320312364301766017 ) ) ;
#4160=ORIENTED_EDGE ( 'NONE', *, *, #5940, .T. ) ;
#4163=CARTESIAN_POINT ( 'NONE',  ( 0.1750025118121568690, 4.719839900820621104, -3.469254087858248070 ) ) ;
#4181=ORIENTED_EDGE ( 'NONE', *, *, #8556, .T. ) ;
#4184=CARTESIAN_POINT ( 'NONE',  ( -2.804994570502171047, -3.229033611042465335, -3.526374918436838701 ) ) ;
#4239=CARTESIAN_POINT ( 'NONE',  ( -4.000000000000000000, 2.511478553582031203, -3.469254451724764543 ) ) ;
#4240=VERTEX_POINT ( 'NONE', #2052 ) ;
#4241=AXIS2_PLACEMENT_3D ( 'NONE', #12986, #806, #1922 ) ;
#4244=DIRECTION ( 'NONE',  ( -0.000000000000000000, -0.000000000000000000, 1.000000000000000000 ) ) ;
#4249=AXIS2_PLACEMENT_3D ( 'NONE', #14349, #14271, #9112 ) ;
#4317=CARTESIAN_POINT ( 'NONE',  ( -4.000000000000000000, 0.000000000000000000, 0.000000000000000000 ) ) ;
#4327=ORIENTED_EDGE ( 'NONE', *, *, #13988, .F. ) ;
#4328=CARTESIAN_POINT ( 'NONE',  ( -6.473970235329672780E-16, -4.862606272033106691, -3.745885042887442395 ) ) ;
#4333=CARTESIAN_POINT ( 'NONE',  ( -4.236525694536558362, 2.416953475386465211, -3.751298745799836354 ) ) ;
#4337=CIRCLE ( 'NONE', #7184, 4.000000000000000000 ) ;
#4351=CONICAL_SURFACE ( 'NONE', #10809, 2.059999999999998721, 0.9599310885968738161 ) ;
#4353=CARTESIAN_POINT ( 'NONE',  ( -5.384454397937118664, 6.594054843588581554E-16, -4.484454397937119197 ) ) ;
#4396=DIRECTION ( 'NONE',  ( -1.000000000000000000, 0.000000000000000000, 0.000000000000000000 ) ) ;
#4398=B_SPLINE_CURVE_WITH_KNOTS ( 'NONE', 3,
 ( #6948, #9363, #13144, #5485, #8082, #6861, #10413, #12978 ),
 .UNSPECIFIED., .F., .F.,
 ( 4, 2, 2, 4 ),
 ( 2.465131517071610173E-07, 0.001183067374689837636, 0.001774477805458902699, 0.002365888236227967761 ),
 .UNSPECIFIED. ) ;
#4409=ORIENTED_EDGE ( 'NONE', *, *, #13196, .T. ) ;
#4413=FACE_OUTER_BOUND ( 'NONE', #847, .T. ) ;
#4434=CARTESIAN_POINT ( 'NONE',  ( 1.567478505476134606E-15, 4.618802153517012066, -3.433295621305382905 ) ) ;
#4438=DIRECTION ( 'NONE',  ( -1.000000000000000000, 0.000000000000000000, 0.000000000000000000 ) ) ;
#4474=CARTESIAN_POINT ( 'NONE',  ( -4.197393957002303999, -0.8151795401431414234, -3.503767560748935139 ) ) ;
#4476=ORIENTED_EDGE ( 'NONE', *, *, #6647, .F. ) ;
#4480=DIRECTION ( 'NONE',  ( -0.000000000000000000, -0.000000000000000000, 1.000000000000000000 ) ) ;
#4490=PLANE ( 'NONE',  #3423 ) ;
#4491=CARTESIAN_POINT ( 'NONE',  ( 4.000000000000000000, -1.560351142792952617, -0.2242961665059816367 ) ) ;
#4494=CARTESIAN_POINT ( 'NONE',  ( 0.000000000000000000, 0.000000000000000000, 0.000000000000000000 ) ) ;
#4523=CARTESIAN_POINT ( 'NONE',  ( 4.000000000000000000, -2.309401076758514915, -3.433295621305383349 ) ) ;
#4536=CARTESIAN_POINT ( 'NONE',  ( 4.207491450040567571, -2.029819825146485179, -3.671670828759567407 ) ) ;
#4546=EDGE_CURVE ( 'NONE', #5482, #13690, #7503, .T. ) ;
#4548=CARTESIAN_POINT ( 'NONE',  ( 0.3198814748697593746, 4.434118497892183264, -0.3507732604232499107 ) ) ;
#4555=ORIENTED_EDGE ( 'NONE', *, *, #8556, .F. ) ;
#4559=ORIENTED_EDGE ( 'NONE', *, *, #13542, .T. ) ;
#4561=VECTOR ( 'NONE', #236, 1000.000000000000114 ) ;
#4571=CARTESIAN_POINT ( 'NONE',  ( 3.999999999999999112, -0.7890432684750902093, -0.04868663549882291247 ) ) ;
#4635=CARTESIAN_POINT ( 'NONE',  ( 3.861362476283255685, 2.629030857715988656, -3.671615880910370500 ) ) ;
#4638=DIRECTION ( 'NONE',  ( 1.000000000000000000, 0.000000000000000000, 0.000000000000000000 ) ) ;
#4685=CARTESIAN_POINT ( 'NONE',  ( -2.688821387764050996E-14, -4.618802153517012954, -0.4999999999999995559 ) ) ;
#4696=SHAPE_REPRESENTATION ( 'hex flange nut gradea_iso_ISO - 4161 - M5 - N', ( #3223 ), #5546 ) ;
#4698=VERTEX_POINT ( 'NONE', #1898 ) ;
#4699=CARTESIAN_POINT ( 'NONE',  ( 2.682243648011666703, 3.070208061305304881, -0.04852650426601266831 ) ) ;
#4707=EDGE_CURVE ( 'NONE', #9986, #13690, #8202, .T. ) ;
#4758=CARTESIAN_POINT ( 'NONE',  ( -4.000000000000000888, -1.539600717839011201, -3.300726591567081591 ) ) ;
#4761=CONICAL_SURFACE ( 'NONE', #13776, 2.059999999999998721, 0.9599310885968738161 ) ;
#4777=ORIENTED_EDGE ( 'NONE', *, *, #6737, .T. ) ;
#4792=CARTESIAN_POINT ( 'NONE',  ( 0.6920835326022565237, 4.454600218803884459, -3.597382984111579862 ) ) ;
#4796=ORIENTED_EDGE ( 'NONE', *, *, #1126, .T. ) ;
#4822=DIRECTION ( 'NONE',  ( 0.000000000000000000, 0.000000000000000000, -1.000000000000000000 ) ) ;
#4832=DIRECTION ( 'NONE',  ( 1.000000000000000000, 0.000000000000000000, 0.000000000000000000 ) ) ;
#4852=CARTESIAN_POINT ( 'NONE',  ( 4.000000000000000000, 2.309401076758497151, -3.433295621305379353 ) ) ;
#4874=CIRCLE ( 'NONE', #9271, 2.100000000000000089 ) ;
#4885=CARTESIAN_POINT ( 'NONE',  ( 4.000000000000000000, 0.000000000000000000, 0.000000000000000000 ) ) ;
#4937=ORIENTED_EDGE ( 'NONE', *, *, #6643, .T. ) ;
#4963=DIRECTION ( 'NONE',  ( -1.000000000000000000, 0.000000000000000000, 0.000000000000000000 ) ) ;
#4981=AXIS2_PLACEMENT_3D ( 'NONE', #8139, #7002, #6837 ) ;
#4994=FACE_OUTER_BOUND ( 'NONE', #1406, .T. ) ;
#5005=CARTESIAN_POINT ( 'NONE',  ( 0.000000000000000000, 0.000000000000000000, -5.000000000000000888 ) ) ;
#5013=TOROIDAL_SURFACE ( 'NONE', #4241, 5.384454397937118664, 0.5155456020628804703 ) ;
#5028=ORIENTED_EDGE ( 'NONE', *, *, #4051, .T. ) ;
#5043=CARTESIAN_POINT ( 'NONE',  ( -2.171643655288372443, 3.365003104552320767, 2.541098841762897165E-18 ) ) ;
#5054=CARTESIAN_POINT ( 'NONE',  ( -2.688821387764050996E-14, -4.618802153517012954, -0.4999999999999995559 ) ) ;
#5057=AXIS2_PLACEMENT_3D ( 'NONE', #8786, #6275, #134 ) ;
#5070=DIRECTION ( 'NONE',  ( -0.000000000000000000, -0.000000000000000000, 1.000000000000000000 ) ) ;
#5083=VERTEX_POINT ( 'NONE', #3831 ) ;
#5084=CARTESIAN_POINT ( 'NONE',  ( 3.455068668934414777, -2.624017327439094327, -3.316620875263732504 ) ) ;
#5138=EDGE_CURVE ( 'NONE', #13545, #15626, #2997, .T. ) ;
#5142=ORIENTED_EDGE ( 'NONE', *, *, #3812, .T. ) ;
#5176=CARTESIAN_POINT ( 'NONE',  ( -4.000000000000000000, -2.309401076758515803, -0.4999999999999995559 ) ) ;
#5182=SURFACE_STYLE_USAGE ( .BOTH. , #15042 ) ;
#5197=DIRECTION ( 'NONE',  ( -0.9396926207859138680, 0.000000000000000000, -0.3420201433256536139 ) ) ;
#5226=LINE ( 'NONE', #15087, #994 ) ;
#5241=CARTESIAN_POINT ( 'NONE',  ( 2.712762565639649015, -3.052587955997662306, -3.430618716626630871 ) ) ;
#5245=ADVANCED_FACE ( 'NONE', ( #11654 ), #12563, .F. ) ;
#5250=CARTESIAN_POINT ( 'NONE',  ( -3.349226789952655547, -2.685125164760744809, -0.2236248678334863682 ) ) ;
#5256=ORIENTED_EDGE ( 'NONE', *, *, #3512, .T. ) ;
#5257=ORIENTED_EDGE ( 'NONE', *, *, #6740, .T. ) ;
#5262=EDGE_CURVE ( 'NONE', #5482, #5812, #10458, .T. ) ;
#5277=ORIENTED_EDGE ( 'NONE', *, *, #7751, .F. ) ;
#5284=VECTOR ( 'NONE', #9338, 1000.000000000000000 ) ;
#5287=CARTESIAN_POINT ( 'NONE',  ( 0.6666666666666658525, -4.233901974057276085, -3.300726591567086476 ) ) ;
#5290=VERTEX_POINT ( 'NONE', #4317 ) ;
#5295=EDGE_CURVE ( 'NONE', #7703, #2885, #3796, .T. ) ;
#5310=CARTESIAN_POINT ( 'NONE',  ( -2.756197834950067094, -3.027510591568735254, -3.223146290109809797 ) ) ;
#5316=CARTESIAN_POINT ( 'NONE',  ( 1.411581201560190495E-15, 4.862606272033091592, -3.745885042887436622 ) ) ;
#5318=ORIENTED_EDGE ( 'NONE', *, *, #6737, .F. ) ;
#5327=CARTESIAN_POINT ( 'NONE',  ( 3.522875095019493141, -2.820352903225631369, -3.598441714920572299 ) ) ;
#5329=DIRECTION ( 'NONE',  ( -0.5000000000000016653, 0.8660254037844378194, 0.000000000000000000 ) ) ;
#5335=CARTESIAN_POINT ( 'NONE',  ( -0.3461262719736137305, 4.658553426539289610, -3.671615880910373608 ) ) ;
#5383=CARTESIAN_POINT ( 'NONE',  ( -4.000000000000000000, 2.471528634177585282, -3.686887442155186712 ) ) ;
#5384=ORIENTED_EDGE ( 'NONE', *, *, #15833, .T. ) ;
#5410=CARTESIAN_POINT ( 'NONE',  ( 1.257172072275274388, -3.892973519170983110, -3.433252694550781303 ) ) ;
#5416=EDGE_CURVE ( 'NONE', #5083, #10519, #8981, .T. ) ;
#5428=CARTESIAN_POINT ( 'NONE',  ( 4.211140560182196957, -2.431303136016555122, -3.745885042887436622 ) ) ;
#5473=FACE_OUTER_BOUND ( 'NONE', #12436, .T. ) ;
#5482=VERTEX_POINT ( 'NONE', #7318 ) ;
#5485=CARTESIAN_POINT ( 'NONE',  ( 2.855764796983346177, -2.970025579236428737, -0.09382832055446485575 ) ) ;
#5499=ORIENTED_EDGE ( 'NONE', *, *, #3853, .F. ) ;
#5526=CARTESIAN_POINT ( 'NONE',  ( 0.000000000000000000, 0.000000000000000000, -4.974599999999998801 ) ) ;
#5546=( GEOMETRIC_REPRESENTATION_CONTEXT ( 3 ) GLOBAL_UNCERTAINTY_ASSIGNED_CONTEXT ( ( #2852 ) ) GLOBAL_UNIT_ASSIGNED_CONTEXT ( ( #5957, #14593, #7256 ) ) REPRESENTATION_CONTEXT ( 'NONE', 'WORKASPACE' ) );
#5548=DIRECTION ( 'NONE',  ( 0.5000000000000022204, 0.8660254037844374864, -0.000000000000000000 ) ) ;
#5549=VECTOR ( 'NONE', #11436, 999.9999999999998863 ) ;
#5565=CARTESIAN_POINT ( 'NONE',  ( -1.391697335622809950, -4.043246145443391448, -3.503898532754372575 ) ) ;
#5566=CIRCLE ( 'NONE', #14582, 4.000000000000000000 ) ;
#5575=FACE_OUTER_BOUND ( 'NONE', #11433, .T. ) ;
#5580=CIRCLE ( 'NONE', #9652, 4.000000000000000000 ) ;
#5587=ORIENTED_EDGE ( 'NONE', *, *, #3647, .T. ) ;
#5589=AXIS2_PLACEMENT_3D ( 'NONE', #4353, #8248, #9291 ) ;
#5600=VERTEX_POINT ( 'NONE', #13986 ) ;
#5609=DIRECTION ( 'NONE',  ( 1.000000000000000000, 0.000000000000000000, 0.000000000000000000 ) ) ;
#5615=DIRECTION ( 'NONE',  ( -0.000000000000000000, -0.000000000000000000, 1.000000000000000000 ) ) ;
#5659=EDGE_LOOP ( 'NONE', ( #10325, #12552, #13769, #13014 ) ) ;
#5663=ORIENTED_EDGE ( 'NONE', *, *, #3647, .F. ) ;
#5664=VERTEX_POINT ( 'NONE', #2183 ) ;
#5665=CARTESIAN_POINT ( 'NONE',  ( 2.805705207896068476, -3.226868319750173075, -3.503898532754370354 ) ) ;
#5669=CIRCLE ( 'NONE', #9792, 5.560781378645573980 ) ;
#5670=CARTESIAN_POINT ( 'NONE',  ( -4.000000000000000888, -2.309401076758512694, -3.504269196027526512 ) ) ;
#5673=CARTESIAN_POINT ( 'NONE',  ( 1.287237434362044075, 3.875615274277557809, -3.430618716626812059 ) ) ;
#5700=ADVANCED_FACE ( 'NONE', ( #1055 ), #9550, .F. ) ;
#5701=CARTESIAN_POINT ( 'NONE',  ( -1.243802165048909503, 3.900692638707381921, -3.223146290109805800 ) ) ;
#5702=EDGE_CURVE ( 'NONE', #12489, #8029, #5963, .T. ) ;
#5703=CARTESIAN_POINT ( 'NONE',  ( 4.000000000000000000, 2.309401076758497151, -3.433295621305379353 ) ) ;
#5745=CARTESIAN_POINT ( 'NONE',  ( 1.390230914382191596, 4.043987460488659202, -3.502507215260488582 ) ) ;
#5754=ORIENTED_EDGE ( 'NONE', *, *, #7419, .F. ) ;
#5767=CYLINDRICAL_SURFACE ( 'NONE', #15624, 2.500000000000000444 ) ;
#5774=CARTESIAN_POINT ( 'NONE',  ( 3.999999999999999112, -1.539600717839012978, -3.300726591567080703 ) ) ;
#5789=ORIENTED_EDGE ( 'NONE', *, *, #15734, .F. ) ;
#5794=( GEOMETRIC_REPRESENTATION_CONTEXT ( 3 ) GLOBAL_UNCERTAINTY_ASSIGNED_CONTEXT ( ( #448 ) ) GLOBAL_UNIT_ASSIGNED_CONTEXT ( ( #1256, #10078, #13440 ) ) REPRESENTATION_CONTEXT ( 'NONE', 'WORKASPACE' ) );
#5812=VERTEX_POINT ( 'NONE', #6963 ) ;
#5840=EDGE_CURVE ( 'NONE', #15429, #4698, #9378, .T. ) ;
#5891=ORIENTED_EDGE ( 'NONE', *, *, #5840, .F. ) ;
#5903=B_SPLINE_CURVE_WITH_KNOTS ( 'NONE', 3,
 ( #7131, #5914, #12356, #12186, #10838, #2408 ),
 .UNSPECIFIED., .F., .F.,
 ( 4, 2, 4 ),
 ( 0.000000000000000000, 0.0002095117440854740156, 0.0004190234881709480313 ),
 .UNSPECIFIED. ) ;
#5914=CARTESIAN_POINT ( 'NONE',  ( -6.259644161404862988E-16, -4.618802153517027165, -3.504271511726793076 ) ) ;
#5932=CARTESIAN_POINT ( 'NONE',  ( 4.211140560182196957, 2.431303136016536470, -3.745885042887433514 ) ) ;
#5940=EDGE_CURVE ( 'NONE', #5482, #10782, #7186, .T. ) ;
#5957=( LENGTH_UNIT ( ) NAMED_UNIT ( * ) SI_UNIT ( .MILLI., .METRE. ) );
#5963=B_SPLINE_CURVE_WITH_KNOTS ( 'NONE', 3,
 ( #14478, #13094, #6069, #2032, #4536, #3473 ),
 .UNSPECIFIED., .F., .F.,
 ( 4, 2, 4 ),
 ( 0.002452478801916361129, 0.003676905084148001344, 0.004901331366379641126 ),
 .UNSPECIFIED. ) ;
#5989=DIRECTION ( 'NONE',  ( 0.000000000000000000, 0.000000000000000000, 1.000000000000000000 ) ) ;
#6004=CYLINDRICAL_SURFACE ( 'NONE', #13063, 2.500000000000000444 ) ;
#6061=CARTESIAN_POINT ( 'NONE',  ( 4.024499207728657879, 2.323545700935571556, -3.572172305156506411 ) ) ;
#6062=DIRECTION ( 'NONE',  ( 0.000000000000000000, 0.000000000000000000, -1.000000000000000000 ) ) ;
#6065=CARTESIAN_POINT ( 'NONE',  ( 3.333333333333332593, 2.694301256218250007, -3.300726591567078483 ) ) ;
#6069=CARTESIAN_POINT ( 'NONE',  ( 4.198928548860774157, -0.8158838809860124996, -3.526471437616918170 ) ) ;
#6070=CARTESIAN_POINT ( 'NONE',  ( 5.560781378645573980, 6.809993116116507654E-16, -4.000000000000000000 ) ) ;
#6072=ORIENTED_EDGE ( 'NONE', *, *, #6505, .F. ) ;
#6162=EDGE_LOOP ( 'NONE', ( #11254, #13347, #14303 ) ) ;
#6163=CARTESIAN_POINT ( 'NONE',  ( 2.000000000000008882, 3.464101615137749945, 0.000000000000000000 ) ) ;
#6195=FACE_OUTER_BOUND ( 'NONE', #15435, .T. ) ;
#6205=ORIENTED_EDGE ( 'NONE', *, *, #1057, .T. ) ;
#6253=ORIENTED_EDGE ( 'NONE', *, *, #5138, .T. ) ;
#6272=CARTESIAN_POINT ( 'NONE',  ( 0.000000000000000000, 0.000000000000000000, -4.694516984716113228 ) ) ;
#6275=DIRECTION ( 'NONE',  ( 0.000000000000000000, 0.000000000000000000, 1.000000000000000000 ) ) ;
#6278=VERTEX_POINT ( 'NONE', #2201 ) ;
#6300=CARTESIAN_POINT ( 'NONE',  ( -4.000000000000000000, -0.8382240730041925492, -3.220610619767135141 ) ) ;
#6303=ORIENTED_EDGE ( 'NONE', *, *, #473, .F. ) ;
#6323=COLOUR_RGB ( '', 0.08235294, 0.09019608, 0.10196078) ;
#6334=VECTOR ( 'NONE', #11893, 1000.000000000000227 ) ;
#6336=CARTESIAN_POINT ( 'NONE',  ( 4.000000000000000000, 2.512223110932545023, -3.469391141908803711 ) ) ;
#6364=CIRCLE ( 'NONE', #5589, 0.5155456020628804703 ) ;
#6386=CARTESIAN_POINT ( 'NONE',  ( -4.000000000000000000, -0.7890432684750890990, -0.04868663549882315533 ) ) ;
#6397=FILL_AREA_STYLE ('',( #12274 ) ) ;
#6420=ORIENTED_EDGE ( 'NONE', *, *, #3255, .T. ) ;
#6433=CARTESIAN_POINT ( 'NONE',  ( -0.6666666666666651864, 4.233901974057260098, -3.300726591567081147 ) ) ;
#6448=CARTESIAN_POINT ( 'NONE',  ( -3.333333333333332149, -2.694301256218264218, -3.300726591567082036 ) ) ;
#6469=CARTESIAN_POINT ( 'NONE',  ( 0.000000000000000000, 0.000000000000000000, -4.974599999999998801 ) ) ;
#6478=CARTESIAN_POINT ( 'NONE',  ( 4.000000000000000000, -2.309401076758516691, -0.4999999999999995559 ) ) ;
#6480=ORIENTED_EDGE ( 'NONE', *, *, #2569, .F. ) ;
#6483=CARTESIAN_POINT ( 'NONE',  ( 4.000000000000000000, -2.309401076758514915, -3.433295621305383349 ) ) ;
#6505=EDGE_CURVE ( 'NONE', #5600, #12918, #11337, .T. ) ;
#6512=ORIENTED_EDGE ( 'NONE', *, *, #5416, .F. ) ;
#6541=CONICAL_SURFACE ( 'NONE', #10917, 4.000000000000000000, 0.8911886515913786111 ) ;
#6545=( BOUNDED_SURFACE ( )  B_SPLINE_SURFACE ( 3, 2, ( 
 ( #10681, #14399, #14549 ),
 ( #6975, #7130, #981 ),
 ( #15777, #9318, #8429 ),
 ( #11876, #5673, #5745 ),
 ( #14239, #3161, #8110 ),
 ( #3878, #12355, #173 ) ),
 .UNSPECIFIED., .F., .F., .F. ) 
 B_SPLINE_SURFACE_WITH_KNOTS ( ( 4, 2, 4 ),
 ( 3, 3 ),
 ( 0.02032853247518126225, 0.02278863295364821212, 0.02524873343211516200 ),
 ( 0.000000000000000000, 1.000000000000000000 ),
 .UNSPECIFIED. ) 
 GEOMETRIC_REPRESENTATION_ITEM ( )  RATIONAL_B_SPLINE_SURFACE ( (
 ( 1.000000000000000000, 0.8047781615896835161, 1.000000000000000000),
 ( 1.000000000000000000, 0.8123767586291043008, 1.000000000000000000),
 ( 1.000000000000000000, 0.8190662415562011134, 1.000000000000000000),
 ( 1.000000000000000000, 0.8192361015671398849, 1.000000000000000000),
 ( 1.000000000000000000, 0.8126135807102121689, 1.000000000000000000),
 ( 1.000000000000000000, 0.8047712338318585568, 1.000000000000000000) ) ) 
 REPRESENTATION_ITEM ( '' )  SURFACE ( )  );
#6548=CARTESIAN_POINT ( 'NONE',  ( -4.211140560182196957, 2.431303136016537803, -3.745885042887433514 ) ) ;
#6568=DIRECTION ( 'NONE',  ( -0.000000000000000000, 0.000000000000000000, -1.000000000000000000 ) ) ;
#6580=CIRCLE ( 'NONE', #7392, 2.499999999999999556 ) ;
#6596=CARTESIAN_POINT ( 'NONE',  ( -6.259644161404860030E-16, -4.618802153517027165, -3.433295621305388234 ) ) ;
#6608=CARTESIAN_POINT ( 'NONE',  ( -1.287237434361707233, -3.875615274277397937, -3.430618716626816500 ) ) ;
#6620=ADVANCED_FACE ( 'NONE', ( #3466 ), #1765, .T. ) ;
#6621=DIRECTION ( 'NONE',  ( -0.000000000000000000, -0.000000000000000000, 1.000000000000000000 ) ) ;
#6632=CARTESIAN_POINT ( 'NONE',  ( 4.000000000000000000, 2.309401076758497151, -5.000000000000000000 ) ) ;
#6643=EDGE_CURVE ( 'NONE', #15626, #3401, #10171, .T. ) ;
#6647=EDGE_CURVE ( 'NONE', #678, #7875, #10375, .T. ) ;
#6648=ORIENTED_EDGE ( 'NONE', *, *, #2916, .T. ) ;
#6689=CARTESIAN_POINT ( 'NONE',  ( -2.807080416178626692, 3.225969019225154444, -3.502507215260441065 ) ) ;
#6692=CIRCLE ( 'NONE', #14175, 0.5155456020628804703 ) ;
#6733=CARTESIAN_POINT ( 'NONE',  ( 4.000000000000000000, 2.309401076758497151, -5.000000000000000000 ) ) ;
#6737=EDGE_CURVE ( 'NONE', #11376, #11740, #3038, .T. ) ;
#6740=EDGE_CURVE ( 'NONE', #10519, #9186, #6692, .T. ) ;
#6760=CARTESIAN_POINT ( 'NONE',  ( -4.197312064133472020, -0.8182229787990021874, -3.502518405183886685 ) ) ;
#6785=CARTESIAN_POINT ( 'NONE',  ( 1.567478505476135000E-15, 4.618802153517012954, -3.504269196027527844 ) ) ;
#6837=DIRECTION ( 'NONE',  ( -1.000000000000000000, 0.000000000000000000, 0.000000000000000000 ) ) ;
#6861=CARTESIAN_POINT ( 'NONE',  ( 2.345747346278113987, -3.264484291692503870, -0.01223254789874484924 ) ) ;
#6889=CARTESIAN_POINT ( 'NONE',  ( -4.000000000000000000, -2.309401076758512694, -3.433295621305382461 ) ) ;
#6913=ADVANCED_FACE ( 'NONE', ( #8850 ), #1490, .T. ) ;
#6930=VECTOR ( 'NONE', #5197, 1000.000000000000227 ) ;
#6948=CARTESIAN_POINT ( 'NONE',  ( 4.000000000000000000, -2.309401076758516691, -0.4999999999999995559 ) ) ;
#6962=EDGE_LOOP ( 'NONE', ( #14982, #3680, #13608 ) ) ;
#6963=CARTESIAN_POINT ( 'NONE',  ( -2.100000000000000089, 2.571758278209441957E-16, -0.2800830152838844622 ) ) ;
#6975=CARTESIAN_POINT ( 'NONE',  ( 3.472371940585993855, 2.614027278893175321, -3.320322319201766792 ) ) ;
#6980=( BOUNDED_SURFACE ( )  B_SPLINE_SURFACE ( 3, 2, ( 
 ( #4239, #5383, #3028 ),
 ( #4158, #15249, #12879 ),
 ( #7436, #2939, #12714 ),
 ( #6300, #11214, #6760 ),
 ( #11508, #3782, #9919 ),
 ( #12417, #8729, #11593 ) ),
 .UNSPECIFIED., .F., .F., .F. ) 
 B_SPLINE_SURFACE_WITH_KNOTS ( ( 4, 2, 4 ),
 ( 3, 3 ),
 ( 0.02027752710269158445, 0.02273781595091097299, 0.02519810479913036153 ),
 ( 0.000000000000000000, 1.000000000000000000 ),
 .UNSPECIFIED. ) 
 GEOMETRIC_REPRESENTATION_ITEM ( )  RATIONAL_B_SPLINE_SURFACE ( (
 ( 1.000000000000000000, 0.8047781431712808242, 1.000000000000000000),
 ( 1.000000000000000000, 0.8123773247083928561, 1.000000000000000000),
 ( 1.000000000000000000, 0.8190670192154906326, 1.000000000000000000),
 ( 1.000000000000000000, 0.8192353552912178261, 1.000000000000000000),
 ( 1.000000000000000000, 0.8126132098226825917, 1.000000000000000000),
 ( 1.000000000000000000, 0.8047712465856394770, 1.000000000000000000) ) ) 
 REPRESENTATION_ITEM ( '' )  SURFACE ( )  );
#6986=ADVANCED_FACE ( 'NONE', ( #3340 ), #14670, .T. ) ;
#7002=DIRECTION ( 'NONE',  ( 0.000000000000000000, -0.000000000000000000, 1.000000000000000000 ) ) ;
#7056=CARTESIAN_POINT ( 'NONE',  ( -4.000000000000000000, 0.3987449864459974846, -0.01220643443059782861 ) ) ;
#7058=AXIS2_PLACEMENT_3D ( 'NONE', #7906, #12650, #13702 ) ;
#7093=EDGE_CURVE ( 'NONE', #1580, #8519, #8063, .T. ) ;
#7126=DIRECTION ( 'NONE',  ( -0.8191520442889875797, 1.003171929053519570E-16, 0.5735764363510522656 ) ) ;
#7130=CARTESIAN_POINT ( 'NONE',  ( 3.453038570460273071, 2.625189405340834448, -3.535263753543585352 ) ) ;
#7131=CARTESIAN_POINT ( 'NONE',  ( -6.259644161404860030E-16, -4.618802153517027165, -3.433295621305388234 ) ) ;
#7137=AXIS2_PLACEMENT_3D ( 'NONE', #12413, #14773, #8566 ) ;
#7141=VERTEX_POINT ( 'NONE', #8442 ) ;
#7177=VERTEX_POINT ( 'NONE', #14726 ) ;
#7184=AXIS2_PLACEMENT_3D ( 'NONE', #3969, #6568, #15225 ) ;
#7186=CIRCLE ( 'NONE', #12059, 2.100000000000000089 ) ;
#7244=DIRECTION ( 'NONE',  ( 0.000000000000000000, 0.000000000000000000, -1.000000000000000000 ) ) ;
#7254=ORIENTED_EDGE ( 'NONE', *, *, #2569, .T. ) ;
#7256=( NAMED_UNIT ( * ) SI_UNIT ( $, .STERADIAN. ) SOLID_ANGLE_UNIT ( ) );
#7265=CARTESIAN_POINT ( 'NONE',  ( 0.000000000000000000, 0.000000000000000000, -0.3080913168122742518 ) ) ;
#7269=ORIENTED_EDGE ( 'NONE', *, *, #3853, .T. ) ;
#7280=DIRECTION ( 'NONE',  ( -1.000000000000000000, 0.000000000000000000, 0.000000000000000000 ) ) ;
#7318=CARTESIAN_POINT ( 'NONE',  ( -2.100000000000000089, 2.571758278209441957E-16, -4.694516984716113228 ) ) ;
#7327=ORIENTED_EDGE ( 'NONE', *, *, #12032, .T. ) ;
#7344=DIRECTION ( 'NONE',  ( 0.8660254037844374864, -0.5000000000000018874, 0.000000000000000000 ) ) ;
#7369=CARTESIAN_POINT ( 'NONE',  ( -1.317756351988340180, 3.857995168970202116, -0.04852650426601388955 ) ) ;
#7387=CARTESIAN_POINT ( 'NONE',  ( 4.211405965630455661, 2.460463115436283932, -3.751298928144577882 ) ) ;
#7392=AXIS2_PLACEMENT_3D ( 'NONE', #11591, #3992, #8944 ) ;
#7408=CARTESIAN_POINT ( 'NONE',  ( 0.000000000000000000, 0.000000000000000000, 0.000000000000000000 ) ) ;
#7419=EDGE_CURVE ( 'NONE', #10129, #14753, #5226, .T. ) ;
#7429=B_SPLINE_CURVE_WITH_KNOTS ( 'NONE', 3,
 ( #411, #11544, #337, #5250, #3071, #5176 ),
 .UNSPECIFIED., .F., .F.,
 ( 4, 2, 4 ),
 ( 0.002365888236228001588, 0.003551327329835089319, 0.004736766423442177049 ),
 .UNSPECIFIED. ) ;
#7436=CARTESIAN_POINT ( 'NONE',  ( -4.000000000000000000, 0.8730739991738342143, -3.223134629628428893 ) ) ;
#7466=CIRCLE ( 'NONE', #8501, 2.500000000000000888 ) ;
#7496=FILL_AREA_STYLE ('',( #2625 ) ) ;
#7503=LINE ( 'NONE', #7581, #4561 ) ;
#7522=PLANE ( 'NONE',  #13123 ) ;
#7556=ORIENTED_EDGE ( 'NONE', *, *, #9426, .T. ) ;
#7573=AXIS2_PLACEMENT_3D ( 'NONE', #9067, #13969, #340 ) ;
#7574=FACE_OUTER_BOUND ( 'NONE', #1040, .T. ) ;
#7581=CARTESIAN_POINT ( 'NONE',  ( -2.500000000000000888, 0.000000000000000000, -4.974599999999998801 ) ) ;
#7600=CARTESIAN_POINT ( 'NONE',  ( -4.000000000000000000, -2.309401076758515803, -0.4999999999999995559 ) ) ;
#7612=PRESENTATION_STYLE_ASSIGNMENT (( #5182 ) ) ;
#7626=EDGE_CURVE ( 'NONE', #10782, #5482, #4874, .T. ) ;
#7637=CARTESIAN_POINT ( 'NONE',  ( 0.000000000000000000, 0.000000000000000000, -4.000000000000000000 ) ) ;
#7657=CARTESIAN_POINT ( 'NONE',  ( -4.207491450040567571, 2.029819825146470524, -3.671670828759566074 ) ) ;
#7673=DIRECTION ( 'NONE',  ( -1.000000000000000000, 0.000000000000000000, 0.000000000000000000 ) ) ;
#7679=ORIENTED_EDGE ( 'NONE', *, *, #10064, .T. ) ;
#7684=CARTESIAN_POINT ( 'NONE',  ( -4.000000000000000000, -0.3979232138631226823, -3.896351557369779711E-17 ) ) ;
#7703=VERTEX_POINT ( 'NONE', #11753 ) ;
#7716=CARTESIAN_POINT ( 'NONE',  ( 4.211140560182196957, 2.431303136016536470, -3.745885042887433514 ) ) ;
#7738=CARTESIAN_POINT ( 'NONE',  ( 4.000000000000000000, -2.309401076758514915, -3.433295621305383349 ) ) ;
#7739=DIRECTION ( 'NONE',  ( -0.000000000000000000, -0.000000000000000000, 1.000000000000000000 ) ) ;
#7751=EDGE_CURVE ( 'NONE', #14753, #15272, #14210, .T. ) ;
#7772=FACE_OUTER_BOUND ( 'NONE', #11213, .T. ) ;
#7793=CARTESIAN_POINT ( 'NONE',  ( 4.197393957002303999, 7.772902908466098641E-14, -3.503767560748929810 ) ) ;
#7831=FACE_OUTER_BOUND ( 'NONE', #11358, .T. ) ;
#7858=CARTESIAN_POINT ( 'NONE',  ( 4.154306624731035846, -2.398490048085128556, -3.721999068284417955 ) ) ;
#7875=VERTEX_POINT ( 'NONE', #3503 ) ;
#7892=DIRECTION ( 'NONE',  ( -0.000000000000000000, -0.000000000000000000, 1.000000000000000000 ) ) ;
#7901=ADVANCED_FACE ( 'NONE', ( #9733, #8462 ), #13360, .F. ) ;
#7906=CARTESIAN_POINT ( 'NONE',  ( 0.000000000000000000, 0.000000000000000000, -4.000000000000000000 ) ) ;
#7920=EDGE_CURVE ( 'NONE', #15685, #7141, #10137, .T. ) ;
#8001=VERTEX_POINT ( 'NONE', #12547 ) ;
#8011=B_SPLINE_CURVE_WITH_KNOTS ( 'NONE', 3,
 ( #6548, #15109, #4029, #8980, #13892, #11463, #5335, #12828 ),
 .UNSPECIFIED., .F., .F.,
 ( 4, 2, 2, 4 ),
 ( 0.000000000000000000, 0.002450665683189820997, 0.003675998524784731495, 0.004901331366379641993 ),
 .UNSPECIFIED. ) ;
#8029=VERTEX_POINT ( 'NONE', #214 ) ;
#8046=CARTESIAN_POINT ( 'NONE',  ( 0.6507732100473444525, -4.243078065514795050, -0.2236248678334952777 ) ) ;
#8061=CARTESIAN_POINT ( 'NONE',  ( -1.257172072275743346, 3.892973519171203378, -3.433252694550776862 ) ) ;
#8063=B_SPLINE_CURVE_WITH_KNOTS ( 'NONE', 3,
 ( #8124, #4548, #8287, #15714, #13178, #9403, #13019, #11727 ),
 .UNSPECIFIED., .F., .F.,
 ( 4, 2, 2, 4 ),
 ( 2.465131517075058656E-07, 0.001183067374689851080, 0.001774477805458923299, 0.002365888236227995517 ),
 .UNSPECIFIED. ) ;
#8066=CARTESIAN_POINT ( 'NONE',  ( 0.000000000000000000, 0.000000000000000000, -4.974599999999998801 ) ) ;
#8082=CARTESIAN_POINT ( 'NONE',  ( 2.687328764639642653, -3.067272167851299969, -0.05923475698271395140 ) ) ;
#8093=DIRECTION ( 'NONE',  ( 0.000000000000000000, 0.000000000000000000, -1.000000000000000000 ) ) ;
#8105=CARTESIAN_POINT ( 'NONE',  ( -5.560781378645575757, 6.809993116116508640E-16, -4.000000000000000000 ) ) ;
#8107=CARTESIAN_POINT ( 'NONE',  ( -4.154094228333736538, -2.398367420967545627, -3.721909803043222276 ) ) ;
#8110=CARTESIAN_POINT ( 'NONE',  ( 0.6810597143197052450, 4.461075778259290914, -3.598441714920602053 ) ) ;
#8124=CARTESIAN_POINT ( 'NONE',  ( 1.734723475976807094E-15, 4.618802153517012954, -0.4999999999999995559 ) ) ;
#8125=DIRECTION ( 'NONE',  ( 0.000000000000000000, 0.000000000000000000, 1.000000000000000000 ) ) ;
#8139=CARTESIAN_POINT ( 'NONE',  ( 0.000000000000000000, 0.000000000000000000, -5.000000000000000888 ) ) ;
#8140=CARTESIAN_POINT ( 'NONE',  ( 0.1404048886732821022, 4.699864953788070565, -3.686887068327037387 ) ) ;
#8145=FACE_OUTER_BOUND ( 'NONE', #3370, .T. ) ;
#8159=CARTESIAN_POINT ( 'NONE',  ( -3.510273485745307287, -2.827716139362669967, -3.610536846335890004 ) ) ;
#8177=ORIENTED_EDGE ( 'NONE', *, *, #12035, .F. ) ;
#8183=AXIS2_PLACEMENT_3D ( 'NONE', #7408, #14677, #3676 ) ;
#8202=CIRCLE ( 'NONE', #9978, 2.500000000000000888 ) ;
#8208=CARTESIAN_POINT ( 'NONE',  ( -4.000000000000000000, 2.309401076758498483, -5.000000000000000000 ) ) ;
#8220=EDGE_CURVE ( 'NONE', #678, #15685, #3004, .T. ) ;
#8248=DIRECTION ( 'NONE',  ( 1.224646799147353207E-16, 1.000000000000000000, 0.000000000000000000 ) ) ;
#8252=CARTESIAN_POINT ( 'NONE',  ( -4.000000000000000000, 2.309401076758498483, -0.4999999999999927280 ) ) ;
#8266=ORIENTED_EDGE ( 'NONE', *, *, #10064, .F. ) ;
#8278=EDGE_CURVE ( 'NONE', #4240, #10306, #5903, .T. ) ;
#8287=CARTESIAN_POINT ( 'NONE',  ( 0.6448876103708359731, 4.246476118072354922, -0.2256878752776725616 ) ) ;
#8342=CARTESIAN_POINT ( 'NONE',  ( 8.673617379884035472E-16, 4.618802153517012954, -5.000000000000000000 ) ) ;
#8424=CARTESIAN_POINT ( 'NONE',  ( -2.000000000000007550, -3.464101615137749945, 0.000000000000000000 ) ) ;
#8429=CARTESIAN_POINT ( 'NONE',  ( 2.836893136758676270, 3.208949435745843903, -3.505054077164911241 ) ) ;
#8442=CARTESIAN_POINT ( 'NONE',  ( -4.000000000000000000, 2.309401076758498483, -3.433295621305379353 ) ) ;
#8462=FACE_OUTER_BOUND ( 'NONE', #13084, .T. ) ;
#8472=ORIENTED_EDGE ( 'NONE', *, *, #9830, .T. ) ;
#8501=AXIS2_PLACEMENT_3D ( 'NONE', #6469, #11223, #2650 ) ;
#8519=VERTEX_POINT ( 'NONE', #9449 ) ;
#8536=( BOUNDED_SURFACE ( )  B_SPLINE_SURFACE ( 3, 2, ( 
 ( #10267, #405, #11455 ),
 ( #2816, #10345, #8891 ),
 ( #3945, #5410, #14955 ),
 ( #13716, #5241, #14044 ),
 ( #5084, #13793, #5327 ),
 ( #15103, #9057, #12737 ) ),
 .UNSPECIFIED., .F., .F., .F. ) 
 B_SPLINE_SURFACE_WITH_KNOTS ( ( 4, 2, 4 ),
 ( 3, 3 ),
 ( 0.02032853247518126918, 0.02278863295364821906, 0.02524873343211517240 ),
 ( 0.000000000000000000, 1.000000000000000000 ),
 .UNSPECIFIED. ) 
 GEOMETRIC_REPRESENTATION_ITEM ( )  RATIONAL_B_SPLINE_SURFACE ( (
 ( 1.000000000000000000, 0.8047781615896837382, 1.000000000000000000),
 ( 1.000000000000000000, 0.8123767586289252218, 1.000000000000000000),
 ( 1.000000000000000000, 0.8190662415564388121, 1.000000000000000000),
 ( 1.000000000000000000, 0.8192361015669026303, 1.000000000000000000),
 ( 1.000000000000000000, 0.8126135807103900266, 1.000000000000000000),
 ( 1.000000000000000000, 0.8047712338318593339, 1.000000000000000000) ) ) 
 REPRESENTATION_ITEM ( '' )  SURFACE ( )  );
#8556=EDGE_CURVE ( 'NONE', #6278, #9986, #11779, .T. ) ;
#8566=DIRECTION ( 'NONE',  ( -1.000000000000000000, 0.000000000000000000, 0.000000000000000000 ) ) ;
#8577=CARTESIAN_POINT ( 'NONE',  ( 4.211140560182196957, 2.431303136016536470, -3.745885042887433514 ) ) ;
#8611=CARTESIAN_POINT ( 'NONE',  ( 4.000000000000000000, 0.1981133338132474442, 2.382280164152719704E-17 ) ) ;
#8640=ORIENTED_EDGE ( 'NONE', *, *, #13761, .F. ) ;
#8654=VECTOR ( 'NONE', #12635, 1000.000000000000000 ) ;
#8665=CARTESIAN_POINT ( 'NONE',  ( 1.734723475976807094E-15, 4.618802153517012954, -0.4999999999999995559 ) ) ;
#8679=ADVANCED_FACE ( 'NONE', ( #10662 ), #9757, .T. ) ;
#8729=CARTESIAN_POINT ( 'NONE',  ( -4.000000000000000000, -2.472261339043343220, -3.687027428081192326 ) ) ;
#8747=( LENGTH_UNIT ( ) NAMED_UNIT ( * ) SI_UNIT ( .MILLI., .METRE. ) );
#8763=CARTESIAN_POINT ( 'NONE',  ( 4.203833317240879275, 1.627343821129582979, -3.597273115243889929 ) ) ;
#8776=CARTESIAN_POINT ( 'NONE',  ( -2.000000000000006661, 3.464101615137750834, 0.000000000000000000 ) ) ;
#8786=CARTESIAN_POINT ( 'NONE',  ( 0.000000000000000000, 0.000000000000000000, -5.000000000000000000 ) ) ;
#8799=DIRECTION ( 'NONE',  ( 0.000000000000000000, 0.000000000000000000, -1.000000000000000000 ) ) ;
#8814=ADVANCED_FACE ( 'NONE', ( #3932 ), #10791, .F. ) ;
#8850=FACE_OUTER_BOUND ( 'NONE', #11257, .T. ) ;
#8864=ORIENTED_EDGE ( 'NONE', *, *, #10715, .F. ) ;
#8881=ADVANCED_FACE ( 'NONE', ( #7831 ), #14930, .F. ) ;
#8891=CARTESIAN_POINT ( 'NONE',  ( 0.6640947660595348800, -4.471078309994175548, -3.602146406945708090 ) ) ;
#8908=CIRCLE ( 'NONE', #11716, 4.000000000000000000 ) ;
#8909=AXIS2_PLACEMENT_3D ( 'NONE', #5005, #9934, #14872 ) ;
#8921=ORIENTED_EDGE ( 'NONE', *, *, #12035, .T. ) ;
#8925=ORIENTED_EDGE ( 'NONE', *, *, #7920, .F. ) ;
#8944=DIRECTION ( 'NONE',  ( 1.000000000000000000, 0.000000000000000000, 0.000000000000000000 ) ) ;
#8948=CARTESIAN_POINT ( 'NONE',  ( -0.6666666666666666297, -4.233901974057276973, -3.300726591567087365 ) ) ;
#8960=CARTESIAN_POINT ( 'NONE',  ( -1.274258131565027874, -3.883108878240886241, -3.220599429844051009 ) ) ;
#8980=CARTESIAN_POINT ( 'NONE',  ( -1.747541505913277282, 3.837784562140256650, -3.503702292528906526 ) ) ;
#8981=CIRCLE ( 'NONE', #15946, 5.384454397937118664 ) ;
#8986=APPLICATION_CONTEXT ( 'automotive_design' ) ;
#8993=ORIENTED_EDGE ( 'NONE', *, *, #14598, .T. ) ;
#9032=ORIENTED_EDGE ( 'NONE', *, *, #4051, .F. ) ;
#9033=EDGE_LOOP ( 'NONE', ( #3293, #10984, #5257, #1350 ) ) ;
#9045=CARTESIAN_POINT ( 'NONE',  ( -1.390230914382372118, -4.043987460488664532, -3.502507215260523665 ) ) ;
#9051=ORIENTED_EDGE ( 'NONE', *, *, #15927, .F. ) ;
#9057=CARTESIAN_POINT ( 'NONE',  ( 4.141042297810615835, -2.227970268150433863, -3.687027686973623819 ) ) ;
#9067=CARTESIAN_POINT ( 'NONE',  ( 0.000000000000000000, 0.000000000000000000, -0.2800830152838844622 ) ) ;
#9109=ORIENTED_EDGE ( 'NONE', *, *, #7626, .T. ) ;
#9112=DIRECTION ( 'NONE',  ( 0.000000000000000000, 0.000000000000000000, 1.000000000000000000 ) ) ;
#9117=VECTOR ( 'NONE', #7126, 999.9999999999998863 ) ;
#9148=CARTESIAN_POINT ( 'NONE',  ( 0.6937372685066666156, -4.453844082567737672, -3.610536846335894445 ) ) ;
#9175=DIRECTION ( 'NONE',  ( 0.000000000000000000, 0.000000000000000000, 1.000000000000000000 ) ) ;
#9178=ORIENTED_EDGE ( 'NONE', *, *, #473, .T. ) ;
#9186=VERTEX_POINT ( 'NONE', #10230 ) ;
#9187=CARTESIAN_POINT ( 'NONE',  ( -2.000000000000002665, -3.464101615137770374, -3.142992957459237680 ) ) ;
#9189=CARTESIAN_POINT ( 'NONE',  ( -2.500000000000000888, 0.000000000000000000, -4.974599999999998801 ) ) ;
#9193=ADVANCED_FACE ( 'NONE', ( #6195 ), #4351, .F. ) ;
#9197=CARTESIAN_POINT ( 'NONE',  ( 0.000000000000000000, 0.000000000000000000, -4.694516984716113228 ) ) ;
#9207=EDGE_LOOP ( 'NONE', ( #9537, #3844, #2667, #4476, #8640 ) ) ;
#9232=ORIENTED_EDGE ( 'NONE', *, *, #15833, .F. ) ;
#9244=ORIENTED_EDGE ( 'NONE', *, *, #8278, .F. ) ;
#9257=CARTESIAN_POINT ( 'NONE',  ( 0.000000000000000000, 0.000000000000000000, 3.469446951953614189E-15 ) ) ;
#9271=AXIS2_PLACEMENT_3D ( 'NONE', #9197, #9278, #705 ) ;
#9278=DIRECTION ( 'NONE',  ( -0.000000000000000000, -0.000000000000000000, 1.000000000000000000 ) ) ;
#9291=DIRECTION ( 'NONE',  ( -1.000000000000000000, 1.224646799147352714E-16, 0.000000000000000000 ) ) ;
#9313=EDGE_CURVE ( 'NONE', #5664, #5600, #13571, .T. ) ;
#9318=CARTESIAN_POINT ( 'NONE',  ( 2.742827927723449299, 3.035229711104609596, -3.433252694550591233 ) ) ;
#9338=DIRECTION ( 'NONE',  ( 0.000000000000000000, 0.000000000000000000, 1.000000000000000000 ) ) ;
#9360=EDGE_LOOP ( 'NONE', ( #2162, #972, #12210 ) ) ;
#9363=CARTESIAN_POINT ( 'NONE',  ( 3.680118525130245732, -2.494084732383344605, -0.3507732604232533524 ) ) ;
#9374=DIRECTION ( 'NONE',  ( -0.000000000000000000, -0.000000000000000000, 1.000000000000000000 ) ) ;
#9378=LINE ( 'NONE', #14675, #14402 ) ;
#9403=CARTESIAN_POINT ( 'NONE',  ( 1.654252653721905331, 3.663718938583014229, -0.01223254789873410957 ) ) ;
#9413=MECHANICAL_DESIGN_GEOMETRIC_PRESENTATION_REPRESENTATION('',(#15362),#5794);
#9426=EDGE_CURVE ( 'NONE', #15428, #7875, #3350, .T. ) ;
#9429=DIRECTION ( 'NONE',  ( -0.000000000000000000, 0.000000000000000000, -1.000000000000000000 ) ) ;
#9449=CARTESIAN_POINT ( 'NONE',  ( 2.000000000000008882, 3.464101615137749945, 0.000000000000000000 ) ) ;
#9461=CARTESIAN_POINT ( 'NONE',  ( 0.000000000000000000, 0.000000000000000000, 0.000000000000000000 ) ) ;
#9471=CARTESIAN_POINT ( 'NONE',  ( 0.000000000000000000, 0.000000000000000000, -5.000000000000000000 ) ) ;
#9495=ORIENTED_EDGE ( 'NONE', *, *, #6505, .T. ) ;
#9525=CARTESIAN_POINT ( 'NONE',  ( 2.548804901056335857E-15, 4.736522675502163437, -3.681124513963624612 ) ) ;
#9537=ORIENTED_EDGE ( 'NONE', *, *, #11221, .T. ) ;
#9544=DIRECTION ( 'NONE',  ( 0.000000000000000000, 0.000000000000000000, -1.000000000000000000 ) ) ;
#9550=CYLINDRICAL_SURFACE ( 'NONE', #10017, 2.100000000000000089 ) ;
#9555=CARTESIAN_POINT ( 'NONE',  ( -4.000000000000000000, 0.9868501483902560878, -0.09357334158579519445 ) ) ;
#9586=ORIENTED_EDGE ( 'NONE', *, *, #3512, .F. ) ;
#9592=DIRECTION ( 'NONE',  ( 0.000000000000000000, 0.000000000000000000, -1.000000000000000000 ) ) ;
#9610=CARTESIAN_POINT ( 'NONE',  ( -1.828356344711647319, -3.563200125723192002, -1.076197711133951296E-14 ) ) ;
#9622=CARTESIAN_POINT ( 'NONE',  ( 3.679171394226031122, 2.494631558665830973, -0.3503314178412474389 ) ) ;
#9636=EDGE_LOOP ( 'NONE', ( #15767, #1595, #9244, #14153 ) ) ;
#9643=ADVANCED_FACE ( 'NONE', ( #14471, #13396 ), #14628, .T. ) ;
#9652=AXIS2_PLACEMENT_3D ( 'NONE', #14865, #14780, #3704 ) ;
#9689=CARTESIAN_POINT ( 'NONE',  ( -0.3198814748697807464, -4.434118497892185040, -0.3507732604232532969 ) ) ;
#9715=DIRECTION ( 'NONE',  ( 1.000000000000000000, 0.000000000000000000, 0.000000000000000000 ) ) ;
#9725=ORIENTED_EDGE ( 'NONE', *, *, #15783, .T. ) ;
#9729=CARTESIAN_POINT ( 'NONE',  ( 5.384454397937118664, 0.000000000000000000, -4.484454397937119197 ) ) ;
#9733=FACE_BOUND ( 'NONE', #3233, .T. ) ;
#9745=SHAPE_REPRESENTATION_RELATIONSHIP ( 'NONE' , 'NONE' ,  #4696, #14078 ) ;
#9757=CONICAL_SURFACE ( 'NONE', #3563, 4.000000000000000000, 0.8911886515913786111 ) ;
#9768=AXIS2_PLACEMENT_3D ( 'NONE', #15479, #14414, #4396 ) ;
#9776=DIRECTION ( 'NONE',  ( -1.000000000000000000, 0.000000000000000000, 0.000000000000000000 ) ) ;
#9792=AXIS2_PLACEMENT_3D ( 'NONE', #7637, #12859, #3008 ) ;
#9808=CARTESIAN_POINT ( 'NONE',  ( 4.000000000001088907, 1.658577278524410170, -3.531553309554541720 ) ) ;
#9824=EDGE_LOOP ( 'NONE', ( #10034, #3310, #4181, #15599 ) ) ;
#9830=EDGE_CURVE ( 'NONE', #13690, #9986, #7466, .T. ) ;
#9843=ORIENTED_EDGE ( 'NONE', *, *, #1486, .T. ) ;
#9853=DIRECTION ( 'NONE',  ( 0.000000000000000000, 0.000000000000000000, -1.000000000000000000 ) ) ;
#9885=CARTESIAN_POINT ( 'NONE',  ( 4.000000000000000000, 2.309401076758515803, -0.4999999999999995559 ) ) ;
#9900=SURFACE_SIDE_STYLE ('',( #13610 ) ) ;
#9905=ADVANCED_FACE ( 'NONE', ( #7772 ), #7522, .T. ) ;
#9912=CARTESIAN_POINT ( 'NONE',  ( -3.472371940586054251, -2.614027278893156669, -3.320322319202162031 ) ) ;
#9919=CARTESIAN_POINT ( 'NONE',  ( -4.203934362469166963, -1.640673743454851286, -3.598432614606932756 ) ) ;
#9934=DIRECTION ( 'NONE',  ( 0.000000000000000000, -0.000000000000000000, 1.000000000000000000 ) ) ;
#9935=CARTESIAN_POINT ( 'NONE',  ( 4.000000000000000000, 2.309401076758497151, -3.433295621305379353 ) ) ;
#9969=CARTESIAN_POINT ( 'NONE',  ( 4.000000000000000000, 0.9868501483902631932, -0.09357334158579604100 ) ) ;
#9974=PRODUCT_DEFINITION_CONTEXT ( 'detailed design', #14975, 'design' ) ;
#9978=AXIS2_PLACEMENT_3D ( 'NONE', #8066, #11751, #10573 ) ;
#9986=VERTEX_POINT ( 'NONE', #13064 ) ;
#9992=SURFACE_STYLE_USAGE ( .BOTH. , #9900 ) ;
#10000=DIRECTION ( 'NONE',  ( 0.000000000000000000, 0.000000000000000000, 1.000000000000000000 ) ) ;
#10012=B_SPLINE_CURVE_WITH_KNOTS ( 'NONE', 3,
 ( #10538, #15385, #7056, #3337, #9555, #10688, #11883, #11804 ),
 .UNSPECIFIED., .F., .F.,
 ( 4, 2, 2, 4 ),
 ( 0.005725059856848641743, 0.006314084072593626612, 0.006903108288338611481, 0.008081156719828581220 ),
 .UNSPECIFIED. ) ;
#10017=AXIS2_PLACEMENT_3D ( 'NONE', #9471, #5989, #11880 ) ;
#10034=ORIENTED_EDGE ( 'NONE', *, *, #15783, .F. ) ;
#10064=EDGE_CURVE ( 'NONE', #8029, #10306, #2872, .T. ) ;
#10071=ORIENTED_EDGE ( 'NONE', *, *, #5295, .T. ) ;
#10073=CARTESIAN_POINT ( 'NONE',  ( -4.197393957002303999, 0.4069871074557429025, -3.503767560748926257 ) ) ;
#10075=CARTESIAN_POINT ( 'NONE',  ( -4.000000000000004441, 2.309401076758496263, -3.504269196027523847 ) ) ;
#10078=( NAMED_UNIT ( * ) PLANE_ANGLE_UNIT ( ) SI_UNIT ( $, .RADIAN. ) );
#10090=CARTESIAN_POINT ( 'NONE',  ( -0.5449313310646672903, -4.304185902836978883, -3.316620875263469159 ) ) ;
#10094=FACE_OUTER_BOUND ( 'NONE', #10096, .T. ) ;
#10096=EDGE_LOOP ( 'NONE', ( #3970, #15916, #7679, #15190, #3479, #9495, #11946 ) ) ;
#10129=VERTEX_POINT ( 'NONE', #4523 ) ;
#10137=B_SPLINE_CURVE_WITH_KNOTS ( 'NONE', 3,
 ( #2691, #6433, #14914, #2777, #12627 ),
 .UNSPECIFIED., .F., .F.,
 ( 4, 1, 4 ),
 ( 0.000000000000000000, 0.002309401076758506657, 0.004618802153517013315 ),
 .UNSPECIFIED. ) ;
#10141=B_SPLINE_CURVE_WITH_KNOTS ( 'NONE', 3,
 ( #14237, #8107, #746, #15696, #5670, #6889 ),
 .UNSPECIFIED., .F., .F.,
 ( 4, 2, 4 ),
 ( -3.640115492409406142E-06, 0.0002066546034006526487, 0.0004169493222937146744 ),
 .UNSPECIFIED. ) ;
#10155=CARTESIAN_POINT ( 'NONE',  ( -4.000000000000000000, -2.309401076758512694, -3.433295621305382461 ) ) ;
#10162=B_SPLINE_CURVE_WITH_KNOTS ( 'NONE', 3,
 ( #1577, #10073, #10320, #11589, #7657, #3991 ),
 .UNSPECIFIED., .F., .F.,
 ( 4, 2, 4 ),
 ( 0.002452478801916376308, 0.003676905084148007850, 0.004901331366379639391 ),
 .UNSPECIFIED. ) ;
#10171=B_SPLINE_CURVE_WITH_KNOTS ( 'NONE', 3,
 ( #4685, #9689, #1284, #14629, #3546, #10988, #9610, #8424 ),
 .UNSPECIFIED., .F., .F.,
 ( 4, 2, 2, 4 ),
 ( 2.465131517390770070E-07, 0.001183067374689869946, 0.001774477805458935659, 0.002365888236228001588 ),
 .UNSPECIFIED. ) ;
#10176=DIRECTION ( 'NONE',  ( 1.000000000000000000, 0.000000000000000000, 0.000000000000000000 ) ) ;
#10192=SURFACE_STYLE_FILL_AREA ( #6397 ) ;
#10220=CARTESIAN_POINT ( 'NONE',  ( 3.999999999999999112, 1.941961291383486277, -0.3515519931180248192 ) ) ;
#10222=EDGE_CURVE ( 'NONE', #7141, #15429, #2101, .T. ) ;
#10230=CARTESIAN_POINT ( 'NONE',  ( 5.560781378645575757, 0.000000000000000000, -4.000000000000000000 ) ) ;
#10239=ORIENTED_EDGE ( 'NONE', *, *, #10899, .F. ) ;
#10257=ORIENTED_EDGE ( 'NONE', *, *, #15632, .F. ) ;
#10264=CARTESIAN_POINT ( 'NONE',  ( -2.000000000000006661, 3.464101615137750834, 0.000000000000000000 ) ) ;
#10267=CARTESIAN_POINT ( 'NONE',  ( -0.1750025118121544265, -4.719839900820635314, -3.469254087858253399 ) ) ;
#10292=AXIS2_PLACEMENT_3D ( 'NONE', #15929, #9853, #7280 ) ;
#10306=VERTEX_POINT ( 'NONE', #4328 ) ;
#10320=CARTESIAN_POINT ( 'NONE',  ( -4.198928548860774157, 0.8158838809860065044, -3.526471437616918170 ) ) ;
#10325=ORIENTED_EDGE ( 'NONE', *, *, #5262, .F. ) ;
#10328=CARTESIAN_POINT ( 'NONE',  ( -2.725741868435985094, 3.045094352034055429, -3.220599429844047012 ) ) ;
#10344=ORIENTED_EDGE ( 'NONE', *, *, #6740, .F. ) ;
#10345=CARTESIAN_POINT ( 'NONE',  ( 0.5469614295415388128, -4.303013824935362663, -3.535263753543555598 ) ) ;
#10346=ADVANCED_FACE ( 'NONE', ( #4994 ), #6980, .F. ) ;
#10360=CARTESIAN_POINT ( 'NONE',  ( 1.747541505913279281, -3.837784562140273081, -3.503702292528912299 ) ) ;
#10375=B_SPLINE_CURVE_WITH_KNOTS ( 'NONE', 3,
 ( #4852, #13398, #6061, #14710, #2337, #8577 ),
 .UNSPECIFIED., .F., .F.,
 ( 4, 2, 4 ),
 ( 0.000000000000000000, 0.0002095117440854730670, 0.0004190234881709461339 ),
 .UNSPECIFIED. ) ;
#10396=CARTESIAN_POINT ( 'NONE',  ( -3.522875095019672109, 2.820352903225427532, -3.598441714920591394 ) ) ;
#10408=CARTESIAN_POINT ( 'NONE',  ( 4.000000000000000000, 0.000000000000000000, 0.000000000000000000 ) ) ;
#10413=CARTESIAN_POINT ( 'NONE',  ( 2.171643655288379993, -3.365003104552334978, -1.195831703456429434E-14 ) ) ;
#10433=CARTESIAN_POINT ( 'NONE',  ( -6.473970235329672780E-16, -4.862606272033106691, -3.745885042887442395 ) ) ;
#10458=LINE ( 'NONE', #15392, #10772 ) ;
#10498=AXIS2_PLACEMENT_3D ( 'NONE', #10882, #4822, #2383 ) ;
#10513=CARTESIAN_POINT ( 'NONE',  ( 0.000000000000000000, 0.000000000000000000, 0.000000000000000000 ) ) ;
#10519=VERTEX_POINT ( 'NONE', #10562 ) ;
#10538=CARTESIAN_POINT ( 'NONE',  ( -4.000000000000000000, 0.000000000000000000, 0.000000000000000000 ) ) ;
#10554=CARTESIAN_POINT ( 'NONE',  ( -4.203833317240879275, -1.627343821129593859, -3.597273115243890818 ) ) ;
#10562=CARTESIAN_POINT ( 'NONE',  ( 5.384454397937118664, 0.000000000000000000, -5.000000000000000000 ) ) ;
#10566=CARTESIAN_POINT ( 'NONE',  ( -4.141042297810615835, 2.227970268150415656, -3.687027686973619822 ) ) ;
#10567=B_SPLINE_CURVE_WITH_KNOTS ( 'NONE', 3,
 ( #2417, #96, #7369, #11156, #12278, #8665 ),
 .UNSPECIFIED., .F., .F.,
 ( 4, 2, 4 ),
 ( 0.002365888236227977302, 0.003551327329835078910, 0.004736766423442180518 ),
 .UNSPECIFIED. ) ;
#10573=DIRECTION ( 'NONE',  ( 1.000000000000000000, 0.000000000000000000, 0.000000000000000000 ) ) ;
#10588=CARTESIAN_POINT ( 'NONE',  ( -6.473970235329672780E-16, -4.862606272033106691, -3.745885042887442395 ) ) ;
#10617=ORIENTED_EDGE ( 'NONE', *, *, #6647, .T. ) ;
#10632=EDGE_LOOP ( 'NONE', ( #6303, #9725, #8472, #4555 ) ) ;
#10652=ADVANCED_FACE ( 'NONE', ( #14904 ), #12328, .F. ) ;
#10662=FACE_OUTER_BOUND ( 'NONE', #13652, .T. ) ;
#10679=LINE ( 'NONE', #10757, #9117 ) ;
#10681=CARTESIAN_POINT ( 'NONE',  ( 4.175002511812151873, 2.208363329454889445, -3.469254087858244073 ) ) ;
#10688=CARTESIAN_POINT ( 'NONE',  ( -4.000000000000000888, 1.563622288139195238, -0.2253451193528307472 ) ) ;
#10693=CIRCLE ( 'NONE', #8909, 2.500000000000000444 ) ;
#10704=FACE_OUTER_BOUND ( 'NONE', #9824, .T. ) ;
#10712=CARTESIAN_POINT ( 'NONE',  ( 4.000000000000000888, 1.539600717838996990, -3.300726591567079815 ) ) ;
#10715=EDGE_CURVE ( 'NONE', #9186, #12918, #5669, .T. ) ;
#10730=CARTESIAN_POINT ( 'NONE',  ( 2.500000000000000888, 3.061616997868384127E-16, -4.974599999999998801 ) ) ;
#10735=CARTESIAN_POINT ( 'NONE',  ( -3.974344831685191280E-13, 4.796734841935104576, -3.721909803043223608 ) ) ;
#10757=CARTESIAN_POINT ( 'NONE',  ( -2.059999999999998721, 2.522772406243545965E-16, -0.3080913168122742518 ) ) ;
#10772=VECTOR ( 'NONE', #8125, 1000.000000000000000 ) ;
#10782=VERTEX_POINT ( 'NONE', #360 ) ;
#10784=CARTESIAN_POINT ( 'NONE',  ( 1.567478505476134606E-15, 4.618802153517012066, -5.000000000000000000 ) ) ;
#10791=( BOUNDED_SURFACE ( )  B_SPLINE_SURFACE ( 3, 2, ( 
 ( #13703, #2715, #12409 ),
 ( #9912, #15178, #4008 ),
 ( #5310, #1666, #4095 ),
 ( #8960, #6608, #9045 ),
 ( #10090, #390, #13948 ),
 ( #12651, #14941, #1426 ) ),
 .UNSPECIFIED., .F., .F., .F. ) 
 B_SPLINE_SURFACE_WITH_KNOTS ( ( 4, 2, 4 ),
 ( 3, 3 ),
 ( 0.02032853247518126918, 0.02278863295364821906, 0.02524873343211516893 ),
 ( 0.000000000000000000, 1.000000000000000000 ),
 .UNSPECIFIED. ) 
 GEOMETRIC_REPRESENTATION_ITEM ( )  RATIONAL_B_SPLINE_SURFACE ( (
 ( 1.000000000000000000, 0.8047781615896838492, 1.000000000000000000),
 ( 1.000000000000000000, 0.8123767586288186404, 1.000000000000000000),
 ( 1.000000000000000000, 0.8190662415565814758, 1.000000000000000000),
 ( 1.000000000000000000, 0.8192361015667604107, 1.000000000000000000),
 ( 1.000000000000000000, 0.8126135807104967190, 1.000000000000000000),
 ( 1.000000000000000000, 0.8047712338318580017, 1.000000000000000000) ) ) 
 REPRESENTATION_ITEM ( '' )  SURFACE ( )  );
#10809=AXIS2_PLACEMENT_3D ( 'NONE', #15155, #7739, #13851 ) ;
#10823=EDGE_LOOP ( 'NONE', ( #11805, #9178 ) ) ;
#10838=CARTESIAN_POINT ( 'NONE',  ( -3.264650091097280831E-13, -4.796980096169642493, -3.721999068284424617 ) ) ;
#10882=CARTESIAN_POINT ( 'NONE',  ( 0.000000000000000000, 0.000000000000000000, -0.2800830152838844622 ) ) ;
#10899=EDGE_CURVE ( 'NONE', #5290, #11376, #10012, .T. ) ;
#10917=AXIS2_PLACEMENT_3D ( 'NONE', #1122, #6062, #15930 ) ;
#10931=FACE_OUTER_BOUND ( 'NONE', #10632, .T. ) ;
#10936=CARTESIAN_POINT ( 'NONE',  ( 4.000000000000000000, -1.677850389431204459, -3.535268758346977513 ) ) ;
#10964=FACE_OUTER_BOUND ( 'NONE', #6962, .T. ) ;
#10966=EDGE_CURVE ( 'NONE', #8519, #14655, #14038, .T. ) ;
#10981=CARTESIAN_POINT ( 'NONE',  ( -4.000000000000000000, -2.309401076758512694, -3.433295621305382461 ) ) ;
#10984=ORIENTED_EDGE ( 'NONE', *, *, #5416, .T. ) ;
#10988=CARTESIAN_POINT ( 'NONE',  ( -1.654252653721913102, -3.663718938583024443, -0.01223254789874440342 ) ) ;
#11020=CARTESIAN_POINT ( 'NONE',  ( 4.000000000000000000, 1.680228229147133767, -3.316631783032546021 ) ) ;
#11046=EDGE_CURVE ( 'NONE', #11740, #1580, #10567, .T. ) ;
#11065=ORIENTED_EDGE ( 'NONE', *, *, #14598, .F. ) ;
#11103=ORIENTED_EDGE ( 'NONE', *, *, #1486, .F. ) ;
#11116=CARTESIAN_POINT ( 'NONE',  ( -4.154094228333456762, 2.398367420968013253, -3.721909803043220055 ) ) ;
#11127=FACE_OUTER_BOUND ( 'NONE', #14721, .T. ) ;
#11156=CARTESIAN_POINT ( 'NONE',  ( -0.6507732100473471171, 4.243078065514775510, -0.2236248678334823436 ) ) ;
#11166=CARTESIAN_POINT ( 'NONE',  ( 4.197393957002303999, 0.8151795401431359833, -3.503767560748935139 ) ) ;
#11168=VECTOR ( 'NONE', #572, 1000.000000000000000 ) ;
#11189=CYLINDRICAL_SURFACE ( 'NONE', #5057, 2.100000000000000089 ) ;
#11213=EDGE_LOOP ( 'NONE', ( #9051, #3153, #5587, #4777, #1334 ) ) ;
#11214=CARTESIAN_POINT ( 'NONE',  ( -4.000000000000000000, -0.8232339106130515116, -3.430630286862743183 ) ) ;
#11221=EDGE_CURVE ( 'NONE', #10129, #8029, #11322, .T. ) ;
#11223=DIRECTION ( 'NONE',  ( -0.000000000000000000, -0.000000000000000000, 1.000000000000000000 ) ) ;
#11237=CARTESIAN_POINT ( 'NONE',  ( 4.101954839143059139, -2.368264730582948285, -3.681130640444269631 ) ) ;
#11252=AXIS2_PLACEMENT_3D ( 'NONE', #2890, #6621, #10176 ) ;
#11254=ORIENTED_EDGE ( 'NONE', *, *, #13061, .T. ) ;
#11257=EDGE_LOOP ( 'NONE', ( #13407, #5256, #12973, #1831, #6253 ) ) ;
#11274=CARTESIAN_POINT ( 'NONE',  ( -4.024497503033519941, 2.323544716729375459, -3.572167766733379768 ) ) ;
#11304=CARTESIAN_POINT ( 'NONE',  ( -4.000000000000000000, 0.000000000000000000, 0.000000000000000000 ) ) ;
#11305=( BOUNDED_SURFACE ( )  B_SPLINE_SURFACE ( 3, 2, ( 
 ( #4163, #8140, #11829 ),
 ( #1656, #15409, #15331 ),
 ( #5701, #8061, #463 ),
 ( #10328, #1739, #6689 ),
 ( #11597, #11747, #10396 ),
 ( #14109, #10566, #4333 ) ),
 .UNSPECIFIED., .F., .F., .F. ) 
 B_SPLINE_SURFACE_WITH_KNOTS ( ( 4, 2, 4 ),
 ( 3, 3 ),
 ( 0.02032853247518125531, 0.02278863295364820865, 0.02524873343211516200 ),
 ( 0.000000000000000000, 1.000000000000000000 ),
 .UNSPECIFIED. ) 
 GEOMETRIC_REPRESENTATION_ITEM ( )  RATIONAL_B_SPLINE_SURFACE ( (
 ( 1.000000000000000000, 0.8047781615896836271, 1.000000000000000000),
 ( 1.000000000000000000, 0.8123767586289967202, 1.000000000000000000),
 ( 1.000000000000000000, 0.8190662415563443322, 1.000000000000000000),
 ( 1.000000000000000000, 0.8192361015669982205, 1.000000000000000000),
 ( 1.000000000000000000, 0.8126135807103181952, 1.000000000000000000),
 ( 1.000000000000000000, 0.8047712338318587788, 1.000000000000000000) ) ) 
 REPRESENTATION_ITEM ( '' )  SURFACE ( )  );
#11320=CARTESIAN_POINT ( 'NONE',  ( 4.024499207728657879, -2.323545700935587988, -3.572172305156509964 ) ) ;
#11322=B_SPLINE_CURVE_WITH_KNOTS ( 'NONE', 3,
 ( #6483, #348, #11320, #11237, #7858, #15212 ),
 .UNSPECIFIED., .F., .F.,
 ( 4, 2, 4 ),
 ( 4.336808689942017736E-19, 0.0002095117440854729585, 0.0004190234881709454834 ),
 .UNSPECIFIED. ) ;
#11337=LINE ( 'NONE', #284, #6930 ) ;
#11338=ORIENTED_EDGE ( 'NONE', *, *, #12862, .F. ) ;
#11353=EDGE_LOOP ( 'NONE', ( #14285, #8266, #179, #9586 ) ) ;
#11354=DIRECTION ( 'NONE',  ( -0.000000000000000000, -0.000000000000000000, 1.000000000000000000 ) ) ;
#11358=EDGE_LOOP ( 'NONE', ( #4160, #7327, #1991, #13764 ) ) ;
#11376=VERTEX_POINT ( 'NONE', #2021 ) ;
#11394=ORIENTED_EDGE ( 'NONE', *, *, #14228, .F. ) ;
#11427=DIRECTION ( 'NONE',  ( -1.000000000000000000, 0.000000000000000000, 0.000000000000000000 ) ) ;
#11433=EDGE_LOOP ( 'NONE', ( #8993, #14555, #8864, #10344 ) ) ;
#11436=DIRECTION ( 'NONE',  ( 0.8191520442889875797, 0.000000000000000000, 0.5735764363510522656 ) ) ;
#11455=CARTESIAN_POINT ( 'NONE',  ( -0.02448733951239248641, -4.877042772274742255, -3.751161874094027571 ) ) ;
#11463=CARTESIAN_POINT ( 'NONE',  ( -0.6937372685066653943, 4.453844082567723461, -3.610536846335889116 ) ) ;
#11469=LINE ( 'NONE', #1613, #2196 ) ;
#11478=COLOUR_RGB ( '', 0.08235294, 0.09019608, 0.10196078) ;
#11508=CARTESIAN_POINT ( 'NONE',  ( -4.000000000000000000, -1.680117682357936904, -3.316611593218794951 ) ) ;
#11513=CARTESIAN_POINT ( 'NONE',  ( 0.000000000000000000, 0.000000000000000000, -4.000000000000000000 ) ) ;
#11534=FACE_OUTER_BOUND ( 'NONE', #9033, .T. ) ;
#11544=CARTESIAN_POINT ( 'NONE',  ( -2.344047193898593395, -3.265465875126480455, -1.054683074273691752E-14 ) ) ;
#11552=DIRECTION ( 'NONE',  ( 0.000000000000000000, 0.000000000000000000, 1.000000000000000000 ) ) ;
#11553=ORIENTED_EDGE ( 'NONE', *, *, #12032, .F. ) ;
#11589=CARTESIAN_POINT ( 'NONE',  ( -4.204015924366189871, 1.626724848190922446, -3.610627190413390419 ) ) ;
#11591=CARTESIAN_POINT ( 'NONE',  ( 0.000000000000000000, 0.000000000000000000, 3.469446951953614189E-15 ) ) ;
#11593=CARTESIAN_POINT ( 'NONE',  ( -4.211405944401398038, -2.460460786169389902, -3.751298493805494072 ) ) ;
#11597=CARTESIAN_POINT ( 'NONE',  ( -3.455068668934486276, 2.624017327439035707, -3.316620875263955437 ) ) ;
#11654=FACE_OUTER_BOUND ( 'NONE', #2675, .T. ) ;
#11662=LINE ( 'NONE', #457, #8654 ) ;
#11716=AXIS2_PLACEMENT_3D ( 'NONE', #9461, #11791, #3090 ) ;
#11723=ADVANCED_FACE ( 'NONE', ( #11534 ), #2211, .T. ) ;
#11727=CARTESIAN_POINT ( 'NONE',  ( 2.000000000000008882, 3.464101615137749945, 0.000000000000000000 ) ) ;
#11734=ORIENTED_EDGE ( 'NONE', *, *, #5295, .F. ) ;
#11740=VERTEX_POINT ( 'NONE', #10264 ) ;
#11747=CARTESIAN_POINT ( 'NONE',  ( -3.436319922987618902, 2.634841920961291439, -3.531542292955721862 ) ) ;
#11751=DIRECTION ( 'NONE',  ( -0.000000000000000000, -0.000000000000000000, 1.000000000000000000 ) ) ;
#11753=CARTESIAN_POINT ( 'NONE',  ( 2.499999999999999556, 0.000000000000000000, 3.469446951953614189E-15 ) ) ;
#11779=LINE ( 'NONE', #732, #3037 ) ;
#11790=ORIENTED_EDGE ( 'NONE', *, *, #7093, .T. ) ;
#11791=DIRECTION ( 'NONE',  ( -0.000000000000000000, 0.000000000000000000, -1.000000000000000000 ) ) ;
#11804=CARTESIAN_POINT ( 'NONE',  ( -4.000000000000000000, 2.309401076758498483, -0.4999999999999927280 ) ) ;
#11805=ORIENTED_EDGE ( 'NONE', *, *, #2500, .T. ) ;
#11813=DIRECTION ( 'NONE',  ( -0.000000000000000000, -0.000000000000000000, 1.000000000000000000 ) ) ;
#11815=AXIS2_PLACEMENT_3D ( 'NONE', #8342, #9544, #9776 ) ;
#11823=CARTESIAN_POINT ( 'NONE',  ( 0.000000000000000000, 0.000000000000000000, -25.03750572909317285 ) ) ;
#11829=CARTESIAN_POINT ( 'NONE',  ( 0.02448733951239481094, 4.877042772274728044, -3.751161874094022242 ) ) ;
#11836=EDGE_CURVE ( 'NONE', #10306, #5664, #14612, .T. ) ;
#11838=DIRECTION ( 'NONE',  ( 1.000000000000000000, 0.000000000000000000, 0.000000000000000000 ) ) ;
#11856=EDGE_CURVE ( 'NONE', #14753, #13545, #4398, .T. ) ;
#11876=CARTESIAN_POINT ( 'NONE',  ( 1.274258131564866448, 3.883108878240963513, -3.220599429844046568 ) ) ;
#11880=DIRECTION ( 'NONE',  ( 1.000000000000000000, 0.000000000000000000, 0.000000000000000000 ) ) ;
#11883=CARTESIAN_POINT ( 'NONE',  ( -4.000000000000000000, 1.941961291383472732, -0.3515519931180205448 ) ) ;
#11886=DIRECTION ( 'NONE',  ( -1.000000000000000000, 0.000000000000000000, 0.000000000000000000 ) ) ;
#11893=DIRECTION ( 'NONE',  ( 0.9396926207859138680, 1.150791560227856926E-16, -0.3420201433256536139 ) ) ;
#11897=CARTESIAN_POINT ( 'NONE',  ( 0.000000000000000000, 0.000000000000000000, 0.000000000000000000 ) ) ;
#11906=EDGE_CURVE ( 'NONE', #5083, #12918, #6364, .T. ) ;
#11946=ORIENTED_EDGE ( 'NONE', *, *, #12395, .T. ) ;
#11972=DIRECTION ( 'NONE',  ( 0.000000000000000000, 0.000000000000000000, 1.000000000000000000 ) ) ;
#12006=CARTESIAN_POINT ( 'NONE',  ( 2.290893957444128645E-15, 4.647089433458768681, -3.572167766733382877 ) ) ;
#12008=CONICAL_SURFACE ( 'NONE', #7137, 5.560781378645573980, 1.221730476396046816 ) ;
#12032=EDGE_CURVE ( 'NONE', #10782, #9986, #13443, .T. ) ;
#12035=EDGE_CURVE ( 'NONE', #14017, #5812, #13056, .T. ) ;
#12044=AXIS2_PLACEMENT_3D ( 'NONE', #5526, #14254, #2851 ) ;
#12059=AXIS2_PLACEMENT_3D ( 'NONE', #6272, #11354, #11427 ) ;
#12103=CARTESIAN_POINT ( 'NONE',  ( -4.000000000000000000, 2.309401076758498483, -3.433295621305379353 ) ) ;
#12131=CARTESIAN_POINT ( 'NONE',  ( 1.391697335622810172, 4.043246145443375461, -3.503898532754365913 ) ) ;
#12136=CARTESIAN_POINT ( 'NONE',  ( 4.000000000000000888, 0.8228435280416209752, -3.430609588141487976 ) ) ;
#12155=ORIENTED_EDGE ( 'NONE', *, *, #2599, .F. ) ;
#12166=CARTESIAN_POINT ( 'NONE',  ( -6.259644161404860030E-16, -4.618802153517027165, -5.000000000000000000 ) ) ;
#12174=CARTESIAN_POINT ( 'NONE',  ( -4.000000000000000000, -7.806255641895631925E-15, -3.142992957459232350 ) ) ;
#12183=FACE_OUTER_BOUND ( 'NONE', #817, .T. ) ;
#12186=CARTESIAN_POINT ( 'NONE',  ( -1.240299975428134203E-15, -4.736529461165891242, -3.681130640444276292 ) ) ;
#12210=ORIENTED_EDGE ( 'NONE', *, *, #5138, .F. ) ;
#12211=CARTESIAN_POINT ( 'NONE',  ( 4.203935335434060505, 1.640780671294165272, -3.598452447879202598 ) ) ;
#12274=FILL_AREA_STYLE_COLOUR ( '', #11478 ) ;
#12278=CARTESIAN_POINT ( 'NONE',  ( -0.3208286057739654917, 4.433571671609680465, -0.3503314178412548774 ) ) ;
#12314=CARTESIAN_POINT ( 'NONE',  ( 1.567478505476134606E-15, 4.618802153517012066, -3.433295621305382905 ) ) ;
#12328=( BOUNDED_SURFACE ( )  B_SPLINE_SURFACE ( 3, 2, ( 
 ( #13422, #2360, #13670 ),
 ( #2434, #10936, #1074 ),
 ( #3585, #15875, #2514 ),
 ( #3735, #12136, #39 ),
 ( #11020, #9808, #12211 ),
 ( #6336, #12455, #7387 ) ),
 .UNSPECIFIED., .F., .F., .F. ) 
 B_SPLINE_SURFACE_WITH_KNOTS ( ( 4, 2, 4 ),
 ( 3, 3 ),
 ( 0.02027065861071770947, 0.02273072267836921331, 0.02519078674602071716 ),
 ( 0.000000000000000000, 1.000000000000000000 ),
 .UNSPECIFIED. ) 
 GEOMETRIC_REPRESENTATION_ITEM ( )  RATIONAL_B_SPLINE_SURFACE ( (
 ( 1.000000000000000000, 0.8047781708337304885, 1.000000000000000000),
 ( 1.000000000000000000, 0.8123765190705307671, 1.000000000000000000),
 ( 1.000000000000000000, 0.8190656277163975707, 1.000000000000000000),
 ( 1.000000000000000000, 0.8192366903512159348, 1.000000000000000000),
 ( 1.000000000000000000, 0.8126138454302893610, 1.000000000000000000),
 ( 1.000000000000000000, 0.8047712246031417660, 1.000000000000000000) ) ) 
 REPRESENTATION_ITEM ( '' )  SURFACE ( )  );
#12336=DIRECTION ( 'NONE',  ( -0.5000000000000019984, -0.8660254037844375974, 0.000000000000000000 ) ) ;
#12355=CARTESIAN_POINT ( 'NONE',  ( -0.1410422978106123659, 4.700232962125094893, -3.687027686973624707 ) ) ;
#12356=CARTESIAN_POINT ( 'NONE',  ( -1.240299975428113101E-15, -4.647091401871173311, -3.572172305156514849 ) ) ;
#12370=SHAPE_DEFINITION_REPRESENTATION ( #15585, #4696 ) ;
#12395=EDGE_CURVE ( 'NONE', #12918, #9186, #444, .T. ) ;
#12402=CARTESIAN_POINT ( 'NONE',  ( 2.000000000000005329, -3.464101615137751722, 0.000000000000000000 ) ) ;
#12409=CARTESIAN_POINT ( 'NONE',  ( -4.235886605889389145, -2.417314728048544303, -3.751161874094020909 ) ) ;
#12413=CARTESIAN_POINT ( 'NONE',  ( 0.000000000000000000, 0.000000000000000000, -4.000000000000000000 ) ) ;
#12417=CARTESIAN_POINT ( 'NONE',  ( -4.000000000000000000, -2.512220745329312610, -3.469390707569719901 ) ) ;
#12418=PRODUCT_DEFINITION ( 'UNKNOWN', '', #4050, #9974 ) ;
#12433=ADVANCED_FACE ( 'NONE', ( #3194 ), #11305, .F. ) ;
#12436=EDGE_LOOP ( 'NONE', ( #5142, #13920, #15406, #6072, #5028, #15662, #7556 ) ) ;
#12455=CARTESIAN_POINT ( 'NONE',  ( 3.999999999999998224, 2.472263674411418588, -3.687027874309861897 ) ) ;
#12478=LINE ( 'NONE', #1510, #5549 ) ;
#12489=VERTEX_POINT ( 'NONE', #1375 ) ;
#12497=CARTESIAN_POINT ( 'NONE',  ( -4.000000000000000000, -1.942223658245633811, -0.3516579909967644246 ) ) ;
#12504=CIRCLE ( 'NONE', #2189, 5.384454397937118664 ) ;
#12547=CARTESIAN_POINT ( 'NONE',  ( -2.500000000000000444, 3.061616997868383634E-16, -5.000000000000000888 ) ) ;
#12552=ORIENTED_EDGE ( 'NONE', *, *, #7626, .F. ) ;
#12563=CONICAL_SURFACE ( 'NONE', #12044, 2.500000000000000888, 0.9599310885968785900 ) ;
#12571=CARTESIAN_POINT ( 'NONE',  ( 0.000000000000000000, 0.000000000000000000, -4.974599999999998801 ) ) ;
#12576=FACE_OUTER_BOUND ( 'NONE', #225, .T. ) ;
#12627=CARTESIAN_POINT ( 'NONE',  ( -4.000000000000000000, 2.309401076758498483, -3.433295621305379353 ) ) ;
#12635=DIRECTION ( 'NONE',  ( -0.000000000000000000, -0.000000000000000000, 1.000000000000000000 ) ) ;
#12640=ADVANCED_FACE ( 'NONE', ( #2993 ), #2910, .F. ) ;
#12650=DIRECTION ( 'NONE',  ( 0.000000000000000000, 0.000000000000000000, -1.000000000000000000 ) ) ;
#12651=CARTESIAN_POINT ( 'NONE',  ( 0.1756481739660539498, -4.720212674038995360, -3.469390959564070620 ) ) ;
#12714=CARTESIAN_POINT ( 'NONE',  ( -4.197477534772231955, 0.8522413273724368521, -3.505042416683225692 ) ) ;
#12716=ORIENTED_EDGE ( 'NONE', *, *, #2548, .F. ) ;
#12737=CARTESIAN_POINT ( 'NONE',  ( 4.236525694536557474, -2.416953475386482530, -3.751298745799839462 ) ) ;
#12779=CARTESIAN_POINT ( 'NONE',  ( 2.000000000000005329, -3.464101615137751722, 0.000000000000000000 ) ) ;
#12799=CARTESIAN_POINT ( 'NONE',  ( 4.000000000000000000, -1.084202172485504434E-14, -3.142992957459231906 ) ) ;
#12803=CARTESIAN_POINT ( 'NONE',  ( 4.000000000000000000, 2.309401076758497151, -5.000000000000000000 ) ) ;
#12828=CARTESIAN_POINT ( 'NONE',  ( 1.411581201560190495E-15, 4.862606272033091592, -3.745885042887436622 ) ) ;
#12859=DIRECTION ( 'NONE',  ( -0.000000000000000000, -0.000000000000000000, 1.000000000000000000 ) ) ;
#12862=EDGE_CURVE ( 'NONE', #15272, #13545, #8908, .T. ) ;
#12879=CARTESIAN_POINT ( 'NONE',  ( -4.204114297095464359, 1.660363174096617156, -3.602136431857887011 ) ) ;
#12889=VECTOR ( 'NONE', #9175, 1000.000000000000000 ) ;
#12918=VERTEX_POINT ( 'NONE', #8105 ) ;
#12922=ORIENTED_EDGE ( 'NONE', *, *, #5940, .F. ) ;
#12973=ORIENTED_EDGE ( 'NONE', *, *, #7419, .T. ) ;
#12978=CARTESIAN_POINT ( 'NONE',  ( 2.000000000000005329, -3.464101615137751722, 0.000000000000000000 ) ) ;
#12986=CARTESIAN_POINT ( 'NONE',  ( 0.000000000000000000, 0.000000000000000000, -4.484454397937119197 ) ) ;
#13014=ORIENTED_EDGE ( 'NONE', *, *, #781, .F. ) ;
#13019=CARTESIAN_POINT ( 'NONE',  ( 1.828356344711641102, 3.563200125723180900, -5.433716356636336675E-16 ) ) ;
#13020=CARTESIAN_POINT ( 'NONE',  ( 0.3208286057739604957, -4.433571671609698228, -0.3503314178412692548 ) ) ;
#13032=ORIENTED_EDGE ( 'NONE', *, *, #3255, .F. ) ;
#13056=CIRCLE ( 'NONE', #10498, 2.100000000000000089 ) ;
#13061=EDGE_CURVE ( 'NONE', #11740, #8519, #5580, .T. ) ;
#13063=AXIS2_PLACEMENT_3D ( 'NONE', #15721, #13419, #9715 ) ;
#13064=CARTESIAN_POINT ( 'NONE',  ( 2.500000000000000888, 3.061616997868384127E-16, -4.974599999999998801 ) ) ;
#13084=EDGE_LOOP ( 'NONE', ( #5499, #13032, #11394, #11338, #15301, #4015 ) ) ;
#13094=CARTESIAN_POINT ( 'NONE',  ( 4.197393957002303999, -0.4069871074557456780, -3.503767560748925813 ) ) ;
#13096=ORIENTED_EDGE ( 'NONE', *, *, #4546, .T. ) ;
#13123=AXIS2_PLACEMENT_3D ( 'NONE', #14958, #5329, #2483 ) ;
#13135=ADVANCED_FACE ( 'NONE', ( #2649 ), #8536, .F. ) ;
#13144=CARTESIAN_POINT ( 'NONE',  ( 3.355112389629172576, -2.681727112203168950, -0.2256878752776777242 ) ) ;
#13175=ORIENTED_EDGE ( 'NONE', *, *, #5840, .T. ) ;
#13176=DIRECTION ( 'NONE',  ( -0.000000000000000000, 0.000000000000000000, -1.000000000000000000 ) ) ;
#13178=CARTESIAN_POINT ( 'NONE',  ( 1.312671235360372224, 3.860931062424219462, -0.05923475698270440348 ) ) ;
#13196=EDGE_CURVE ( 'NONE', #4698, #5290, #3958, .T. ) ;
#13347=ORIENTED_EDGE ( 'NONE', *, *, #7093, .F. ) ;
#13360=PLANE ( 'NONE',  #1253 ) ;
#13396=FACE_OUTER_BOUND ( 'NONE', #2743, .T. ) ;
#13398=CARTESIAN_POINT ( 'NONE',  ( 3.999999999999999112, 2.309401076758497595, -3.504271511726784194 ) ) ;
#13407=ORIENTED_EDGE ( 'NONE', *, *, #2916, .F. ) ;
#13408=ORIENTED_EDGE ( 'NONE', *, *, #10966, .F. ) ;
#13409=CARTESIAN_POINT ( 'NONE',  ( 2.344047193898588954, 3.265465875126468021, -5.031375706690542042E-16 ) ) ;
#13419=DIRECTION ( 'NONE',  ( -0.000000000000000000, -0.000000000000000000, 1.000000000000000000 ) ) ;
#13421=ORIENTED_EDGE ( 'NONE', *, *, #8220, .T. ) ;
#13422=CARTESIAN_POINT ( 'NONE',  ( 4.000000000000000000, -2.511475576507276042, -3.469253905236643565 ) ) ;
#13440=( NAMED_UNIT ( * ) SI_UNIT ( $, .STERADIAN. ) SOLID_ANGLE_UNIT ( ) );
#13443=LINE ( 'NONE', #10730, #171 ) ;
#13480=CARTESIAN_POINT ( 'NONE',  ( 4.000000000000000000, 2.309401076758515803, -0.4999999999999995559 ) ) ;
#13503=CARTESIAN_POINT ( 'NONE',  ( -3.680118525130244400, 2.494084732383327285, -0.3507732604232449702 ) ) ;
#13524=MECHANICAL_DESIGN_GEOMETRIC_PRESENTATION_REPRESENTATION('',(#398),#410);
#13542=EDGE_CURVE ( 'NONE', #14017, #7703, #12478, .T. ) ;
#13545=VERTEX_POINT ( 'NONE', #12402 ) ;
#13556=CARTESIAN_POINT ( 'NONE',  ( 2.000000000000000444, 3.464101615137754830, -3.142992957459231018 ) ) ;
#13571=B_SPLINE_CURVE_WITH_KNOTS ( 'NONE', 3,
 ( #15557, #10554, #4474, #14006 ),
 .UNSPECIFIED., .F., .F.,
 ( 4, 4 ),
 ( 0.000000000000000000, 0.002452478801916376308 ),
 .UNSPECIFIED. ) ;
#13608=ORIENTED_EDGE ( 'NONE', *, *, #11856, .F. ) ;
#13610=SURFACE_STYLE_FILL_AREA ( #7496 ) ;
#13617=CARTESIAN_POINT ( 'NONE',  ( 0.000000000000000000, 0.000000000000000000, 0.000000000000000000 ) ) ;
#13652=EDGE_LOOP ( 'NONE', ( #10239, #7269, #5318 ) ) ;
#13670=CARTESIAN_POINT ( 'NONE',  ( 4.211399257449709665, -2.459727064652517114, -3.751161691472417736 ) ) ;
#13690=VERTEX_POINT ( 'NONE', #9189 ) ;
#13702=DIRECTION ( 'NONE',  ( -1.000000000000000000, 0.000000000000000000, 0.000000000000000000 ) ) ;
#13703=CARTESIAN_POINT ( 'NONE',  ( -4.175002511812151873, -2.208363329454905877, -3.469254087858246738 ) ) ;
#13716=CARTESIAN_POINT ( 'NONE',  ( 2.725741868436127202, -3.045094352033990148, -3.220599429844051453 ) ) ;
#13761=EDGE_CURVE ( 'NONE', #10129, #678, #1151, .T. ) ;
#13764=ORIENTED_EDGE ( 'NONE', *, *, #4546, .F. ) ;
#13769=ORIENTED_EDGE ( 'NONE', *, *, #14844, .T. ) ;
#13776=AXIS2_PLACEMENT_3D ( 'NONE', #7265, #5070, #4832 ) ;
#13782=ADVANCED_FACE ( 'NONE', ( #4413 ), #15570, .T. ) ;
#13793=CARTESIAN_POINT ( 'NONE',  ( 3.436319922986518449, -2.634841920959471562, -3.531542292954761741 ) ) ;
#13847=DIRECTION ( 'NONE',  ( 0.000000000000000000, 0.000000000000000000, -1.000000000000000000 ) ) ;
#13851=DIRECTION ( 'NONE',  ( 1.000000000000000000, 0.000000000000000000, 0.000000000000000000 ) ) ;
#13892=CARTESIAN_POINT ( 'NONE',  ( -1.393927851585477606, 4.043713361053528743, -3.526374918436835149 ) ) ;
#13920=ORIENTED_EDGE ( 'NONE', *, *, #14575, .T. ) ;
#13948=CARTESIAN_POINT ( 'NONE',  ( -0.6810597143197697489, -4.461075778259609770, -3.598441714920717516 ) ) ;
#13969=DIRECTION ( 'NONE',  ( 0.000000000000000000, 0.000000000000000000, -1.000000000000000000 ) ) ;
#13986=CARTESIAN_POINT ( 'NONE',  ( -4.197393957002303999, -7.773935952363655451E-14, -3.503767560748929810 ) ) ;
#13988=EDGE_CURVE ( 'NONE', #15272, #14655, #2699, .T. ) ;
#14003=CONICAL_SURFACE ( 'NONE', #7058, 5.560781378645573980, 1.221730476396046816 ) ;
#14004=CARTESIAN_POINT ( 'NONE',  ( -6.259644161404860030E-16, -4.618802153517027165, -3.433295621305388234 ) ) ;
#14006=CARTESIAN_POINT ( 'NONE',  ( -4.197393957002303999, -7.773935952363655451E-14, -3.503767560748929810 ) ) ;
#14017=VERTEX_POINT ( 'NONE', #1565 ) ;
#14038=B_SPLINE_CURVE_WITH_KNOTS ( 'NONE', 3,
 ( #6163, #13409, #4699, #14884, #9622, #13480 ),
 .UNSPECIFIED., .F., .F.,
 ( 4, 2, 4 ),
 ( 0.002365888236227995517, 0.003551327329835084114, 0.004736766423442172712 ),
 .UNSPECIFIED. ) ;
#14044=CARTESIAN_POINT ( 'NONE',  ( 2.807080416178989513, -3.225969019225150003, -3.502507215260505014 ) ) ;
#14078=ADVANCED_BREP_SHAPE_REPRESENTATION ( '', ( #14732, #3223 ), #5546 ) ;
#14109=CARTESIAN_POINT ( 'NONE',  ( -4.175648173966055587, 2.207990556236529844, -3.469390959564062626 ) ) ;
#14153=ORIENTED_EDGE ( 'NONE', *, *, #316, .F. ) ;
#14175=AXIS2_PLACEMENT_3D ( 'NONE', #9729, #121, #7244 ) ;
#14185=LINE ( 'NONE', #6070, #6334 ) ;
#14210=B_SPLINE_CURVE_WITH_KNOTS ( 'NONE', 3,
 ( #1900, #14275, #4491, #4571, #14437, #14583 ),
 .UNSPECIFIED., .F., .F.,
 ( 4, 2, 4 ),
 ( 0.003358874760055551890, 0.004541967308452098118, 0.005725059856848645212 ),
 .UNSPECIFIED. ) ;
#14228=EDGE_CURVE ( 'NONE', #13545, #3401, #5566, .T. ) ;
#14237=CARTESIAN_POINT ( 'NONE',  ( -4.211140560182196957, -2.431303136016552013, -3.745885042887436178 ) ) ;
#14239=CARTESIAN_POINT ( 'NONE',  ( 0.5449313310647804220, 4.304185902836899835, -3.316620875263383894 ) ) ;
#14254=DIRECTION ( 'NONE',  ( 0.000000000000000000, 0.000000000000000000, -1.000000000000000000 ) ) ;
#14271=DIRECTION ( 'NONE',  ( -1.000000000000000000, 0.000000000000000000, 0.000000000000000000 ) ) ;
#14275=CARTESIAN_POINT ( 'NONE',  ( 4.000000000000000000, -1.942223658245635809, -0.3516579909967643691 ) ) ;
#14276=DIRECTION ( 'NONE',  ( -0.000000000000000000, -0.000000000000000000, 1.000000000000000000 ) ) ;
#14285=ORIENTED_EDGE ( 'NONE', *, *, #8278, .T. ) ;
#14288=CARTESIAN_POINT ( 'NONE',  ( -0.6920835326022555245, -4.454600218803899558, -3.597382984111586079 ) ) ;
#14301=DIRECTION ( 'NONE',  ( 0.000000000000000000, 0.000000000000000000, 1.000000000000000000 ) ) ;
#14303=ORIENTED_EDGE ( 'NONE', *, *, #11046, .F. ) ;
#14349=CARTESIAN_POINT ( 'NONE',  ( -4.000000000000000000, 2.309401076758498483, -5.000000000000000000 ) ) ;
#14383=ORIENTED_EDGE ( 'NONE', *, *, #13542, .F. ) ;
#14389=CARTESIAN_POINT ( 'NONE',  ( 1.393927851585479161, -4.043713361053543842, -3.526374918436840922 ) ) ;
#14399=CARTESIAN_POINT ( 'NONE',  ( 4.140404888673277384, 2.228338276487440428, -3.686887068327033390 ) ) ;
#14402=VECTOR ( 'NONE', #14301, 1000.000000000000000 ) ;
#14414=DIRECTION ( 'NONE',  ( 0.000000000000000000, 0.000000000000000000, -1.000000000000000000 ) ) ;
#14437=CARTESIAN_POINT ( 'NONE',  ( 3.999999999999999112, -0.3979232138631231819, -5.929230630780099908E-17 ) ) ;
#14449=PRODUCT_CONTEXT ( 'NONE', #8986, 'mechanical' ) ;
#14471=FACE_BOUND ( 'NONE', #10823, .T. ) ;
#14478=CARTESIAN_POINT ( 'NONE',  ( 4.197393957002303999, 7.772902908466098641E-14, -3.503767560748929810 ) ) ;
#14525=AXIS2_PLACEMENT_3D ( 'NONE', #13617, #9592, #14690 ) ;
#14549=CARTESIAN_POINT ( 'NONE',  ( 4.235886605889389145, 2.417314728048528760, -3.751161874094018245 ) ) ;
#14555=ORIENTED_EDGE ( 'NONE', *, *, #11906, .T. ) ;
#14575=EDGE_CURVE ( 'NONE', #12489, #9186, #14185, .T. ) ;
#14582=AXIS2_PLACEMENT_3D ( 'NONE', #3406, #13176, #11886 ) ;
#14583=CARTESIAN_POINT ( 'NONE',  ( 4.000000000000000000, 0.000000000000000000, 0.000000000000000000 ) ) ;
#14593=( NAMED_UNIT ( * ) PLANE_ANGLE_UNIT ( ) SI_UNIT ( $, .RADIAN. ) );
#14598=EDGE_CURVE ( 'NONE', #10519, #5083, #12504, .T. ) ;
#14612=B_SPLINE_CURVE_WITH_KNOTS ( 'NONE', 3,
 ( #10588, #14288, #5565, #3059, #4184, #8159, #876, #3210 ),
 .UNSPECIFIED., .F., .F.,
 ( 4, 2, 2, 4 ),
 ( 0.000000000000000000, 0.002450665683189818828, 0.003675998524784728459, 0.004901331366379638524 ),
 .UNSPECIFIED. ) ;
#14628=PLANE ( 'NONE',  #11815 ) ;
#14629=CARTESIAN_POINT ( 'NONE',  ( -1.144235203016679359, -3.958177651039096911, -0.09382832055446428676 ) ) ;
#14655=VERTEX_POINT ( 'NONE', #3111 ) ;
#14670=CONICAL_SURFACE ( 'NONE', #9768, 4.000000000000000000, 0.8911886515913786111 ) ;
#14675=CARTESIAN_POINT ( 'NONE',  ( -4.000000000000000000, -2.309401076758512694, -5.000000000000000000 ) ) ;
#14677=DIRECTION ( 'NONE',  ( 0.000000000000000000, 0.000000000000000000, -1.000000000000000000 ) ) ;
#14690=DIRECTION ( 'NONE',  ( -1.000000000000000000, 0.000000000000000000, 0.000000000000000000 ) ) ;
#14710=CARTESIAN_POINT ( 'NONE',  ( 4.101954839143060028, 2.368264730582927857, -3.681130640444267854 ) ) ;
#14721=EDGE_LOOP ( 'NONE', ( #2586, #154, #4559, #10071 ) ) ;
#14726=CARTESIAN_POINT ( 'NONE',  ( -4.211140560182196957, 2.431303136016537803, -3.745885042887433514 ) ) ;
#14732=MANIFOLD_SOLID_BREP ( 'EndChamfer', #3261 ) ;
#14753=VERTEX_POINT ( 'NONE', #6478 ) ;
#14773=DIRECTION ( 'NONE',  ( 0.000000000000000000, 0.000000000000000000, -1.000000000000000000 ) ) ;
#14780=DIRECTION ( 'NONE',  ( -0.000000000000000000, 0.000000000000000000, -1.000000000000000000 ) ) ;
#14801=VECTOR ( 'NONE', #1104, 1000.000000000000000 ) ;
#14822=CARTESIAN_POINT ( 'NONE',  ( -2.855764796983342624, 2.970025579236414082, -0.09382832055445475272 ) ) ;
#14844=EDGE_CURVE ( 'NONE', #10782, #14017, #11469, .T. ) ;
#14855=ORIENTED_EDGE ( 'NONE', *, *, #10899, .T. ) ;
#14865=CARTESIAN_POINT ( 'NONE',  ( 0.000000000000000000, 0.000000000000000000, 0.000000000000000000 ) ) ;
#14866=AXIS2_PLACEMENT_3D ( 'NONE', #15323, #7892, #1731 ) ;
#14872=DIRECTION ( 'NONE',  ( -1.000000000000000000, 0.000000000000000000, 0.000000000000000000 ) ) ;
#14874=CARTESIAN_POINT ( 'NONE',  ( 1.567478505476134606E-15, 4.618802153517012066, -3.433295621305382905 ) ) ;
#14884=CARTESIAN_POINT ( 'NONE',  ( 3.349226789952652439, 2.685125164760731487, -0.2236248678334773199 ) ) ;
#14904=FACE_OUTER_BOUND ( 'NONE', #9207, .T. ) ;
#14905=AXIS2_PLACEMENT_3D ( 'NONE', #9257, #11813, #5609 ) ;
#14910=CARTESIAN_POINT ( 'NONE',  ( 4.000000000000000888, 1.563622288139206118, -0.2253451193528334950 ) ) ;
#14914=CARTESIAN_POINT ( 'NONE',  ( -1.999999999999999556, 3.464101615137754830, -3.142992957459232795 ) ) ;
#14930=CONICAL_SURFACE ( 'NONE', #15954, 2.500000000000000888, 0.9599310885968785900 ) ;
#14941=CARTESIAN_POINT ( 'NONE',  ( 0.1410422978106145031, -4.700232962125109104, -3.687027686973628704 ) ) ;
#14955=CARTESIAN_POINT ( 'NONE',  ( 1.360585162435110629, -4.061296242128317857, -3.505054077164905024 ) ) ;
#14958=CARTESIAN_POINT ( 'NONE',  ( 1.567478505476134606E-15, 4.618802153517012066, -5.000000000000000000 ) ) ;
#14975=APPLICATION_CONTEXT ( 'automotive_design' ) ;
#14982=ORIENTED_EDGE ( 'NONE', *, *, #7751, .T. ) ;
#15042=SURFACE_SIDE_STYLE ('',( #10192 ) ) ;
#15049=DIRECTION ( 'NONE',  ( -1.000000000000000000, 0.000000000000000000, 0.000000000000000000 ) ) ;
#15068=CARTESIAN_POINT ( 'NONE',  ( 1.999999999999998224, -3.464101615137772594, -3.142992957459239012 ) ) ;
#15083=B_SPLINE_CURVE_WITH_KNOTS ( 'NONE', 3,
 ( #3602, #11116, #3843, #11274, #10075, #3916 ),
 .UNSPECIFIED., .F., .F.,
 ( 4, 2, 4 ),
 ( -3.640115492410698714E-06, 0.0002066546034006521879, 0.0004169493222937151081 ),
 .UNSPECIFIED. ) ;
#15087=CARTESIAN_POINT ( 'NONE',  ( 4.000000000000000000, -2.309401076758514915, -5.000000000000000000 ) ) ;
#15103=CARTESIAN_POINT ( 'NONE',  ( 4.175648173966055587, -2.207990556236547608, -3.469390959564065291 ) ) ;
#15109=CARTESIAN_POINT ( 'NONE',  ( -3.511755186886750479, 2.826662030176366081, -3.597382984111578086 ) ) ;
#15117=ADVANCED_FACE ( 'NONE', ( #12576 ), #2559, .T. ) ;
#15155=CARTESIAN_POINT ( 'NONE',  ( 0.000000000000000000, 0.000000000000000000, -0.3080913168122742518 ) ) ;
#15178=CARTESIAN_POINT ( 'NONE',  ( -3.453038570459499024, -2.625189405340453419, -3.535263753545272891 ) ) ;
#15183=CARTESIAN_POINT ( 'NONE',  ( -4.000000000000000000, -2.309401076758512694, -3.433295621305382461 ) ) ;
#15190=ORIENTED_EDGE ( 'NONE', *, *, #11836, .T. ) ;
#15212=CARTESIAN_POINT ( 'NONE',  ( 4.211140560182196957, -2.431303136016555122, -3.745885042887436622 ) ) ;
#15225=DIRECTION ( 'NONE',  ( -1.000000000000000000, 0.000000000000000000, 0.000000000000000000 ) ) ;
#15235=ADVANCED_FACE ( 'NONE', ( #10094 ), #12008, .T. ) ;
#15249=CARTESIAN_POINT ( 'NONE',  ( -4.000000000000000000, 1.677772373332757194, -3.535253723897187506 ) ) ;
#15272=VERTEX_POINT ( 'NONE', #10408 ) ;
#15290=ORIENTED_EDGE ( 'NONE', *, *, #10222, .F. ) ;
#15301=ORIENTED_EDGE ( 'NONE', *, *, #15734, .T. ) ;
#15312=CARTESIAN_POINT ( 'NONE',  ( 1.317756351988342622, -3.857995168970215438, -0.04852650426602527628 ) ) ;
#15322=CIRCLE ( 'NONE', #4981, 2.500000000000000444 ) ;
#15323=CARTESIAN_POINT ( 'NONE',  ( 0.000000000000000000, 0.000000000000000000, 0.000000000000000000 ) ) ;
#15331=CARTESIAN_POINT ( 'NONE',  ( -0.6640947660597427138, 4.471078309994878985, -3.602146406945963442 ) ) ;
#15346=ORIENTED_EDGE ( 'NONE', *, *, #14844, .F. ) ;
#15362=STYLED_ITEM ( 'NONE', ( #137 ), #14078 ) ;
#15385=CARTESIAN_POINT ( 'NONE',  ( -4.000000000000000000, 0.1981133338132459731, 2.096406544454392723E-17 ) ) ;
#15392=CARTESIAN_POINT ( 'NONE',  ( -2.100000000000000089, 2.571758278209441957E-16, -5.000000000000000000 ) ) ;
#15406=ORIENTED_EDGE ( 'NONE', *, *, #10715, .T. ) ;
#15409=CARTESIAN_POINT ( 'NONE',  ( -0.5469614295416921346, 4.303013824936271270, -3.535263753543735454 ) ) ;
#15428=VERTEX_POINT ( 'NONE', #5316 ) ;
#15429=VERTEX_POINT ( 'NONE', #15183 ) ;
#15435=EDGE_LOOP ( 'NONE', ( #8921, #4796, #5384, #14383 ) ) ;
#15479=CARTESIAN_POINT ( 'NONE',  ( 0.000000000000000000, 0.000000000000000000, 0.000000000000000000 ) ) ;
#15501=CARTESIAN_POINT ( 'NONE',  ( 0.000000000000000000, 0.000000000000000000, -5.000000000000000000 ) ) ;
#15554=CARTESIAN_POINT ( 'NONE',  ( 1.655952806101427033, -3.662737355149048302, -1.182683869819604841E-14 ) ) ;
#15557=CARTESIAN_POINT ( 'NONE',  ( -4.211140560182196957, -2.431303136016552013, -3.745885042887436178 ) ) ;
#15570=PLANE ( 'NONE',  #4249 ) ;
#15585=PRODUCT_DEFINITION_SHAPE ( 'NONE', 'NONE',  #12418 ) ;
#15595=ADVANCED_FACE ( 'NONE', ( #2377 ), #2209, .T. ) ;
#15599=ORIENTED_EDGE ( 'NONE', *, *, #4707, .T. ) ;
#15614=ADVANCED_FACE ( 'NONE', ( #7574 ), #11189, .F. ) ;
#15624=AXIS2_PLACEMENT_3D ( 'NONE', #11823, #4480, #3416 ) ;
#15626=VERTEX_POINT ( 'NONE', #5054 ) ;
#15632=EDGE_CURVE ( 'NONE', #7177, #7141, #15083, .T. ) ;
#15662=ORIENTED_EDGE ( 'NONE', *, *, #2599, .T. ) ;
#15673=CARTESIAN_POINT ( 'NONE',  ( 1.411581201560190495E-15, 4.862606272033091592, -3.745885042887436622 ) ) ;
#15685=VERTEX_POINT ( 'NONE', #12314 ) ;
#15696=CARTESIAN_POINT ( 'NONE',  ( -4.024497503033519941, -2.323544716729390558, -3.572167766733381544 ) ) ;
#15711=CIRCLE ( 'NONE', #1511, 4.000000000000000000 ) ;
#15714=CARTESIAN_POINT ( 'NONE',  ( 1.144235203016666258, 3.958177651039090250, -0.09382832055445661235 ) ) ;
#15721=CARTESIAN_POINT ( 'NONE',  ( 0.000000000000000000, 0.000000000000000000, -25.03750572909317285 ) ) ;
#15734=EDGE_CURVE ( 'NONE', #15272, #8519, #1701, .T. ) ;
#15767=ORIENTED_EDGE ( 'NONE', *, *, #1057, .F. ) ;
#15777=CARTESIAN_POINT ( 'NONE',  ( 2.756197834950227410, 3.027510591568626896, -3.223146290109805356 ) ) ;
#15783=EDGE_CURVE ( 'NONE', #8001, #13690, #11662, .T. ) ;
#15833=EDGE_CURVE ( 'NONE', #2885, #7703, #6580, .T. ) ;
#15875=CARTESIAN_POINT ( 'NONE',  ( 4.000000000000000888, -0.8578082829538523635, -3.433262215449808696 ) ) ;
#15916=ORIENTED_EDGE ( 'NONE', *, *, #5702, .T. ) ;
#15927=EDGE_CURVE ( 'NONE', #15685, #1580, #2053, .T. ) ;
#15929=CARTESIAN_POINT ( 'NONE',  ( 0.000000000000000000, 0.000000000000000000, 0.000000000000000000 ) ) ;
#15930=DIRECTION ( 'NONE',  ( -1.000000000000000000, 0.000000000000000000, 0.000000000000000000 ) ) ;
#15946=AXIS2_PLACEMENT_3D ( 'NONE', #15501, #14276, #11838 ) ;
#15947=ADVANCED_FACE ( 'NONE', ( #10704 ), #5767, .F. ) ;
#15954=AXIS2_PLACEMENT_3D ( 'NONE', #12571, #8799, #7673 ) ;
ENDSEC;
END-ISO-10303-21;
